ISO-10303-21;
HEADER;
/* Generated by software containing ST-Developer
 * from STEP Tools, Inc. (www.steptools.com) 
 */

FILE_DESCRIPTION(
/* description */ (''),
/* implementation_level */ '2;1');

FILE_NAME(
/* name */ 'Bracket_02 (1).step',
/* time_stamp */ '2026-10-22T15:07:41+06:00',
/* author */ (''),
/* organization */ (''),
/* preprocessor_version */ 'ST-DEVELOPER v20.2',
/* originating_system */ 'Autodesk Translation Framework v15.15.0.0',
/* authorisation */ '');

FILE_SCHEMA (('AUTOMOTIVE_DESIGN { 1 0 10303 214 3 1 1 }'));
ENDSEC;

DATA;
#10=MECHANICAL_DESIGN_GEOMETRIC_PRESENTATION_REPRESENTATION('',(#2886),#19220);
#75=SHAPE_REPRESENTATION_RELATIONSHIP('SRR','None',#19278,#89);
#89=ADVANCED_BREP_SHAPE_REPRESENTATION('',(#103),#19214);
#103=MANIFOLD_SOLID_BREP('Bracket_02',#11322);
#567=FACE_BOUND('',#4321,.T.);
#568=FACE_BOUND('',#4322,.T.);
#569=FACE_BOUND('',#4323,.T.);
#570=FACE_BOUND('',#4324,.T.);
#571=FACE_BOUND('',#4325,.T.);
#572=FACE_BOUND('',#4326,.T.);
#573=FACE_BOUND('',#4327,.T.);
#574=FACE_BOUND('',#4328,.T.);
#575=FACE_BOUND('',#4329,.T.);
#576=FACE_BOUND('',#4330,.T.);
#577=FACE_BOUND('',#4331,.T.);
#578=FACE_BOUND('',#4334,.T.);
#579=FACE_BOUND('',#4335,.T.);
#580=FACE_BOUND('',#4336,.T.);
#581=FACE_BOUND('',#4337,.T.);
#582=FACE_BOUND('',#4338,.T.);
#583=FACE_BOUND('',#4339,.T.);
#584=FACE_BOUND('',#4340,.T.);
#585=FACE_BOUND('',#4341,.T.);
#586=FACE_BOUND('',#4342,.T.);
#587=FACE_BOUND('',#4343,.T.);
#588=FACE_BOUND('',#4344,.T.);
#589=FACE_BOUND('',#4362,.T.);
#590=FACE_BOUND('',#4363,.T.);
#591=FACE_BOUND('',#4364,.T.);
#592=FACE_BOUND('',#4365,.T.);
#593=FACE_BOUND('',#4366,.T.);
#594=FACE_BOUND('',#4367,.T.);
#595=FACE_BOUND('',#4368,.T.);
#596=FACE_BOUND('',#4369,.T.);
#597=FACE_BOUND('',#4370,.T.);
#598=FACE_BOUND('',#4371,.T.);
#599=FACE_BOUND('',#4372,.T.);
#600=FACE_BOUND('',#4390,.T.);
#601=FACE_BOUND('',#4391,.T.);
#602=FACE_BOUND('',#4392,.T.);
#603=FACE_BOUND('',#4393,.T.);
#604=FACE_BOUND('',#4394,.T.);
#605=FACE_BOUND('',#4395,.T.);
#606=FACE_BOUND('',#4396,.T.);
#607=FACE_BOUND('',#4397,.T.);
#608=FACE_BOUND('',#4398,.T.);
#609=FACE_BOUND('',#4399,.T.);
#610=FACE_BOUND('',#4400,.T.);
#611=FACE_BOUND('',#4402,.T.);
#612=FACE_BOUND('',#4403,.T.);
#613=FACE_BOUND('',#4404,.T.);
#614=FACE_BOUND('',#4406,.T.);
#615=FACE_BOUND('',#4409,.T.);
#616=FACE_BOUND('',#4410,.T.);
#760=PLANE('',#12501);
#761=PLANE('',#12516);
#762=PLANE('',#12539);
#763=PLANE('',#12540);
#764=PLANE('',#12541);
#765=PLANE('',#12542);
#766=PLANE('',#12543);
#767=PLANE('',#12544);
#768=PLANE('',#12578);
#769=PLANE('',#12579);
#770=PLANE('',#12580);
#771=PLANE('',#12581);
#772=PLANE('',#12582);
#773=PLANE('',#12583);
#774=PLANE('',#12584);
#775=PLANE('',#12585);
#776=PLANE('',#12586);
#777=PLANE('',#12587);
#778=PLANE('',#12588);
#779=PLANE('',#12589);
#1449=LINE('',#18483,#2304);
#1450=LINE('',#18489,#2305);
#1451=LINE('',#18495,#2306);
#1452=LINE('',#18502,#2307);
#1453=LINE('',#18505,#2308);
#1454=LINE('',#18508,#2309);
#1455=LINE('',#18510,#2310);
#1456=LINE('',#18512,#2311);
#1457=LINE('',#18514,#2312);
#1458=LINE('',#18516,#2313);
#1459=LINE('',#18518,#2314);
#1460=LINE('',#18519,#2315);
#1461=LINE('',#18547,#2316);
#1462=LINE('',#18550,#2317);
#1463=LINE('',#18553,#2318);
#1464=LINE('',#18555,#2319);
#1465=LINE('',#18557,#2320);
#1466=LINE('',#18559,#2321);
#1467=LINE('',#18561,#2322);
#1468=LINE('',#18563,#2323);
#1469=LINE('',#18564,#2324);
#1470=LINE('',#18588,#2325);
#1471=LINE('',#18590,#2326);
#1472=LINE('',#18592,#2327);
#1473=LINE('',#18594,#2328);
#1474=LINE('',#18596,#2329);
#1475=LINE('',#18598,#2330);
#1476=LINE('',#18600,#2331);
#1477=LINE('',#18602,#2332);
#1478=LINE('',#18604,#2333);
#1479=LINE('',#18606,#2334);
#1480=LINE('',#18608,#2335);
#1481=LINE('',#18610,#2336);
#1482=LINE('',#18611,#2337);
#1483=LINE('',#18613,#2338);
#1484=LINE('',#18614,#2339);
#1485=LINE('',#18616,#2340);
#1486=LINE('',#18618,#2341);
#1487=LINE('',#18623,#2342);
#1488=LINE('',#18625,#2343);
#1489=LINE('',#18627,#2344);
#1490=LINE('',#18629,#2345);
#1491=LINE('',#18631,#2346);
#1492=LINE('',#18633,#2347);
#1493=LINE('',#18635,#2348);
#1494=LINE('',#18636,#2349);
#1495=LINE('',#18662,#2350);
#1496=LINE('',#18666,#2351);
#1497=LINE('',#18670,#2352);
#1498=LINE('',#18674,#2353);
#1499=LINE('',#18678,#2354);
#1500=LINE('',#18682,#2355);
#1501=LINE('',#18686,#2356);
#1502=LINE('',#18690,#2357);
#1503=LINE('',#18694,#2358);
#1504=LINE('',#18698,#2359);
#1505=LINE('',#18702,#2360);
#1506=LINE('',#18705,#2361);
#1507=LINE('',#18707,#2362);
#1508=LINE('',#18708,#2363);
#1509=LINE('',#18711,#2364);
#1510=LINE('',#18713,#2365);
#1511=LINE('',#18714,#2366);
#1512=LINE('',#18717,#2367);
#1513=LINE('',#18718,#2368);
#1514=LINE('',#18721,#2369);
#1515=LINE('',#18722,#2370);
#1516=LINE('',#18724,#2371);
#1517=LINE('',#18728,#2372);
#1518=LINE('',#18729,#2373);
#1519=LINE('',#18730,#2374);
#1520=LINE('',#18733,#2375);
#1521=LINE('',#18735,#2376);
#1522=LINE('',#18736,#2377);
#1523=LINE('',#18738,#2378);
#1524=LINE('',#18739,#2379);
#1525=LINE('',#18742,#2380);
#1526=LINE('',#18743,#2381);
#1527=LINE('',#18746,#2382);
#1528=LINE('',#18747,#2383);
#1529=LINE('',#18749,#2384);
#2304=VECTOR('',#15354,1.5);
#2305=VECTOR('',#15361,2.00000000000003);
#2306=VECTOR('',#15368,2.00000000000003);
#2307=VECTOR('',#15375,10.);
#2308=VECTOR('',#15378,10.);
#2309=VECTOR('',#15381,10.);
#2310=VECTOR('',#15382,10.);
#2311=VECTOR('',#15383,10.);
#2312=VECTOR('',#15384,10.);
#2313=VECTOR('',#15385,10.);
#2314=VECTOR('',#15386,10.);
#2315=VECTOR('',#15387,10.);
#2316=VECTOR('',#15414,4.);
#2317=VECTOR('',#15417,10.);
#2318=VECTOR('',#15420,10.);
#2319=VECTOR('',#15421,10.);
#2320=VECTOR('',#15422,10.);
#2321=VECTOR('',#15423,10.);
#2322=VECTOR('',#15424,10.);
#2323=VECTOR('',#15425,10.);
#2324=VECTOR('',#15426,10.);
#2325=VECTOR('',#15451,1.49999999999999);
#2326=VECTOR('',#15454,1.49999999999999);
#2327=VECTOR('',#15457,1.49999999999999);
#2328=VECTOR('',#15460,1.49999999999999);
#2329=VECTOR('',#15463,1.49999999999999);
#2330=VECTOR('',#15466,1.49999999999999);
#2331=VECTOR('',#15469,1.49999999999999);
#2332=VECTOR('',#15472,1.49999999999999);
#2333=VECTOR('',#15475,1.49999999999999);
#2334=VECTOR('',#15478,1.49999999999999);
#2335=VECTOR('',#15481,1.49999999999999);
#2336=VECTOR('',#15484,10.);
#2337=VECTOR('',#15485,10.);
#2338=VECTOR('',#15488,10.);
#2339=VECTOR('',#15489,10.);
#2340=VECTOR('',#15492,10.);
#2341=VECTOR('',#15495,10.);
#2342=VECTOR('',#15500,10.);
#2343=VECTOR('',#15501,10.);
#2344=VECTOR('',#15502,10.);
#2345=VECTOR('',#15503,10.);
#2346=VECTOR('',#15504,10.);
#2347=VECTOR('',#15505,10.);
#2348=VECTOR('',#15506,10.);
#2349=VECTOR('',#15507,10.);
#2350=VECTOR('',#15534,1.49999999999999);
#2351=VECTOR('',#15539,1.49999999999999);
#2352=VECTOR('',#15544,1.49999999999999);
#2353=VECTOR('',#15549,1.49999999999999);
#2354=VECTOR('',#15554,1.49999999999999);
#2355=VECTOR('',#15559,1.49999999999999);
#2356=VECTOR('',#15564,1.49999999999999);
#2357=VECTOR('',#15569,1.49999999999999);
#2358=VECTOR('',#15574,1.49999999999999);
#2359=VECTOR('',#15579,1.49999999999999);
#2360=VECTOR('',#15584,1.49999999999999);
#2361=VECTOR('',#15587,10.);
#2362=VECTOR('',#15588,10.);
#2363=VECTOR('',#15589,10.);
#2364=VECTOR('',#15592,10.);
#2365=VECTOR('',#15593,10.);
#2366=VECTOR('',#15594,10.);
#2367=VECTOR('',#15597,10.);
#2368=VECTOR('',#15598,10.);
#2369=VECTOR('',#15601,10.);
#2370=VECTOR('',#15602,10.);
#2371=VECTOR('',#15605,10.);
#2372=VECTOR('',#15608,10.);
#2373=VECTOR('',#15609,10.);
#2374=VECTOR('',#15610,10.);
#2375=VECTOR('',#15613,10.);
#2376=VECTOR('',#15614,10.);
#2377=VECTOR('',#15615,10.);
#2378=VECTOR('',#15618,10.);
#2379=VECTOR('',#15619,10.);
#2380=VECTOR('',#15622,10.);
#2381=VECTOR('',#15623,10.);
#2382=VECTOR('',#15626,10.);
#2383=VECTOR('',#15627,10.);
#2384=VECTOR('',#15630,10.);
#2829=CYLINDRICAL_SURFACE('',#12489,1.5);
#2830=CYLINDRICAL_SURFACE('',#12492,2.00000000000003);
#2831=CYLINDRICAL_SURFACE('',#12495,2.00000000000003);
#2832=CYLINDRICAL_SURFACE('',#12498,2.);
#2833=CYLINDRICAL_SURFACE('',#12513,4.);
#2834=CYLINDRICAL_SURFACE('',#12528,1.49999999999999);
#2835=CYLINDRICAL_SURFACE('',#12529,1.49999999999999);
#2836=CYLINDRICAL_SURFACE('',#12530,1.49999999999999);
#2837=CYLINDRICAL_SURFACE('',#12531,1.49999999999999);
#2838=CYLINDRICAL_SURFACE('',#12532,1.49999999999999);
#2839=CYLINDRICAL_SURFACE('',#12533,1.49999999999999);
#2840=CYLINDRICAL_SURFACE('',#12534,1.49999999999999);
#2841=CYLINDRICAL_SURFACE('',#12535,1.49999999999999);
#2842=CYLINDRICAL_SURFACE('',#12536,1.49999999999999);
#2843=CYLINDRICAL_SURFACE('',#12537,1.49999999999999);
#2844=CYLINDRICAL_SURFACE('',#12538,1.49999999999999);
#2845=CYLINDRICAL_SURFACE('',#12556,1.49999999999999);
#2846=CYLINDRICAL_SURFACE('',#12558,1.49999999999999);
#2847=CYLINDRICAL_SURFACE('',#12560,1.49999999999999);
#2848=CYLINDRICAL_SURFACE('',#12562,1.49999999999999);
#2849=CYLINDRICAL_SURFACE('',#12564,1.49999999999999);
#2850=CYLINDRICAL_SURFACE('',#12566,1.49999999999999);
#2851=CYLINDRICAL_SURFACE('',#12568,1.49999999999999);
#2852=CYLINDRICAL_SURFACE('',#12570,1.49999999999999);
#2853=CYLINDRICAL_SURFACE('',#12572,1.49999999999999);
#2854=CYLINDRICAL_SURFACE('',#12574,1.49999999999999);
#2855=CYLINDRICAL_SURFACE('',#12576,1.49999999999999);
#2886=STYLED_ITEM('',(#19382),#103);
#3312=FACE_OUTER_BOUND('',#4316,.T.);
#3313=FACE_OUTER_BOUND('',#4317,.T.);
#3314=FACE_OUTER_BOUND('',#4318,.T.);
#3315=FACE_OUTER_BOUND('',#4319,.T.);
#3316=FACE_OUTER_BOUND('',#4320,.T.);
#3317=FACE_OUTER_BOUND('',#4332,.T.);
#3318=FACE_OUTER_BOUND('',#4333,.T.);
#3319=FACE_OUTER_BOUND('',#4345,.T.);
#3320=FACE_OUTER_BOUND('',#4346,.T.);
#3321=FACE_OUTER_BOUND('',#4347,.T.);
#3322=FACE_OUTER_BOUND('',#4348,.T.);
#3323=FACE_OUTER_BOUND('',#4349,.T.);
#3324=FACE_OUTER_BOUND('',#4350,.T.);
#3325=FACE_OUTER_BOUND('',#4351,.T.);
#3326=FACE_OUTER_BOUND('',#4352,.T.);
#3327=FACE_OUTER_BOUND('',#4353,.T.);
#3328=FACE_OUTER_BOUND('',#4354,.T.);
#3329=FACE_OUTER_BOUND('',#4355,.T.);
#3330=FACE_OUTER_BOUND('',#4356,.T.);
#3331=FACE_OUTER_BOUND('',#4357,.T.);
#3332=FACE_OUTER_BOUND('',#4358,.T.);
#3333=FACE_OUTER_BOUND('',#4359,.T.);
#3334=FACE_OUTER_BOUND('',#4360,.T.);
#3335=FACE_OUTER_BOUND('',#4361,.T.);
#3336=FACE_OUTER_BOUND('',#4373,.T.);
#3337=FACE_OUTER_BOUND('',#4374,.T.);
#3338=FACE_OUTER_BOUND('',#4375,.T.);
#3339=FACE_OUTER_BOUND('',#4376,.T.);
#3340=FACE_OUTER_BOUND('',#4377,.T.);
#3341=FACE_OUTER_BOUND('',#4378,.T.);
#3342=FACE_OUTER_BOUND('',#4379,.T.);
#3343=FACE_OUTER_BOUND('',#4380,.T.);
#3344=FACE_OUTER_BOUND('',#4381,.T.);
#3345=FACE_OUTER_BOUND('',#4382,.T.);
#3346=FACE_OUTER_BOUND('',#4383,.T.);
#3347=FACE_OUTER_BOUND('',#4384,.T.);
#3348=FACE_OUTER_BOUND('',#4385,.T.);
#3349=FACE_OUTER_BOUND('',#4386,.T.);
#3350=FACE_OUTER_BOUND('',#4387,.T.);
#3351=FACE_OUTER_BOUND('',#4388,.T.);
#3352=FACE_OUTER_BOUND('',#4389,.T.);
#3353=FACE_OUTER_BOUND('',#4401,.T.);
#3354=FACE_OUTER_BOUND('',#4405,.T.);
#3355=FACE_OUTER_BOUND('',#4407,.T.);
#3356=FACE_OUTER_BOUND('',#4408,.T.);
#3357=FACE_OUTER_BOUND('',#4411,.T.);
#3358=FACE_OUTER_BOUND('',#4412,.T.);
#4316=EDGE_LOOP('',(#10084,#10085,#10086,#10087));
#4317=EDGE_LOOP('',(#10088,#10089,#10090,#10091));
#4318=EDGE_LOOP('',(#10092,#10093,#10094,#10095));
#4319=EDGE_LOOP('',(#10096,#10097,#10098,#10099));
#4320=EDGE_LOOP('',(#10100,#10101,#10102,#10103,#10104,#10105,#10106,#10107));
#4321=EDGE_LOOP('',(#10108));
#4322=EDGE_LOOP('',(#10109));
#4323=EDGE_LOOP('',(#10110));
#4324=EDGE_LOOP('',(#10111));
#4325=EDGE_LOOP('',(#10112));
#4326=EDGE_LOOP('',(#10113));
#4327=EDGE_LOOP('',(#10114));
#4328=EDGE_LOOP('',(#10115));
#4329=EDGE_LOOP('',(#10116));
#4330=EDGE_LOOP('',(#10117));
#4331=EDGE_LOOP('',(#10118));
#4332=EDGE_LOOP('',(#10119,#10120,#10121,#10122));
#4333=EDGE_LOOP('',(#10123,#10124,#10125,#10126,#10127,#10128,#10129,#10130));
#4334=EDGE_LOOP('',(#10131));
#4335=EDGE_LOOP('',(#10132));
#4336=EDGE_LOOP('',(#10133));
#4337=EDGE_LOOP('',(#10134));
#4338=EDGE_LOOP('',(#10135));
#4339=EDGE_LOOP('',(#10136));
#4340=EDGE_LOOP('',(#10137));
#4341=EDGE_LOOP('',(#10138));
#4342=EDGE_LOOP('',(#10139));
#4343=EDGE_LOOP('',(#10140));
#4344=EDGE_LOOP('',(#10141));
#4345=EDGE_LOOP('',(#10142,#10143,#10144,#10145));
#4346=EDGE_LOOP('',(#10146,#10147,#10148,#10149));
#4347=EDGE_LOOP('',(#10150,#10151,#10152,#10153));
#4348=EDGE_LOOP('',(#10154,#10155,#10156,#10157));
#4349=EDGE_LOOP('',(#10158,#10159,#10160,#10161));
#4350=EDGE_LOOP('',(#10162,#10163,#10164,#10165));
#4351=EDGE_LOOP('',(#10166,#10167,#10168,#10169));
#4352=EDGE_LOOP('',(#10170,#10171,#10172,#10173));
#4353=EDGE_LOOP('',(#10174,#10175,#10176,#10177));
#4354=EDGE_LOOP('',(#10178,#10179,#10180,#10181));
#4355=EDGE_LOOP('',(#10182,#10183,#10184,#10185));
#4356=EDGE_LOOP('',(#10186,#10187,#10188,#10189));
#4357=EDGE_LOOP('',(#10190,#10191,#10192,#10193));
#4358=EDGE_LOOP('',(#10194,#10195,#10196,#10197));
#4359=EDGE_LOOP('',(#10198,#10199,#10200,#10201));
#4360=EDGE_LOOP('',(#10202,#10203,#10204,#10205));
#4361=EDGE_LOOP('',(#10206,#10207,#10208,#10209,#10210,#10211,#10212,#10213));
#4362=EDGE_LOOP('',(#10214));
#4363=EDGE_LOOP('',(#10215));
#4364=EDGE_LOOP('',(#10216));
#4365=EDGE_LOOP('',(#10217));
#4366=EDGE_LOOP('',(#10218));
#4367=EDGE_LOOP('',(#10219));
#4368=EDGE_LOOP('',(#10220));
#4369=EDGE_LOOP('',(#10221));
#4370=EDGE_LOOP('',(#10222));
#4371=EDGE_LOOP('',(#10223));
#4372=EDGE_LOOP('',(#10224));
#4373=EDGE_LOOP('',(#10225,#10226,#10227,#10228));
#4374=EDGE_LOOP('',(#10229,#10230,#10231,#10232));
#4375=EDGE_LOOP('',(#10233,#10234,#10235,#10236));
#4376=EDGE_LOOP('',(#10237,#10238,#10239,#10240));
#4377=EDGE_LOOP('',(#10241,#10242,#10243,#10244));
#4378=EDGE_LOOP('',(#10245,#10246,#10247,#10248));
#4379=EDGE_LOOP('',(#10249,#10250,#10251,#10252));
#4380=EDGE_LOOP('',(#10253,#10254,#10255,#10256));
#4381=EDGE_LOOP('',(#10257,#10258,#10259,#10260));
#4382=EDGE_LOOP('',(#10261,#10262,#10263,#10264));
#4383=EDGE_LOOP('',(#10265,#10266,#10267,#10268));
#4384=EDGE_LOOP('',(#10269,#10270,#10271,#10272));
#4385=EDGE_LOOP('',(#10273,#10274,#10275,#10276));
#4386=EDGE_LOOP('',(#10277,#10278,#10279,#10280));
#4387=EDGE_LOOP('',(#10281,#10282,#10283,#10284));
#4388=EDGE_LOOP('',(#10285,#10286,#10287,#10288));
#4389=EDGE_LOOP('',(#10289,#10290,#10291,#10292,#10293,#10294,#10295,#10296));
#4390=EDGE_LOOP('',(#10297));
#4391=EDGE_LOOP('',(#10298));
#4392=EDGE_LOOP('',(#10299));
#4393=EDGE_LOOP('',(#10300));
#4394=EDGE_LOOP('',(#10301));
#4395=EDGE_LOOP('',(#10302));
#4396=EDGE_LOOP('',(#10303));
#4397=EDGE_LOOP('',(#10304));
#4398=EDGE_LOOP('',(#10305));
#4399=EDGE_LOOP('',(#10306));
#4400=EDGE_LOOP('',(#10307));
#4401=EDGE_LOOP('',(#10308,#10309,#10310,#10311));
#4402=EDGE_LOOP('',(#10312));
#4403=EDGE_LOOP('',(#10313));
#4404=EDGE_LOOP('',(#10314));
#4405=EDGE_LOOP('',(#10315,#10316,#10317,#10318));
#4406=EDGE_LOOP('',(#10319));
#4407=EDGE_LOOP('',(#10320,#10321,#10322,#10323,#10324,#10325,#10326,#10327,
#10328,#10329,#10330,#10331));
#4408=EDGE_LOOP('',(#10332,#10333,#10334,#10335));
#4409=EDGE_LOOP('',(#10336));
#4410=EDGE_LOOP('',(#10337));
#4411=EDGE_LOOP('',(#10338,#10339,#10340,#10341,#10342,#10343,#10344,#10345,
#10346,#10347,#10348,#10349));
#4412=EDGE_LOOP('',(#10350,#10351,#10352,#10353));
#5077=CIRCLE('',#12490,1.5);
#5078=CIRCLE('',#12491,1.5);
#5079=CIRCLE('',#12493,2.00000000000003);
#5080=CIRCLE('',#12494,2.00000000000003);
#5081=CIRCLE('',#12496,2.00000000000003);
#5082=CIRCLE('',#12497,2.00000000000003);
#5083=CIRCLE('',#12499,2.);
#5084=CIRCLE('',#12500,2.);
#5085=CIRCLE('',#12502,1.49999999999999);
#5086=CIRCLE('',#12503,1.49999999999999);
#5087=CIRCLE('',#12504,1.49999999999999);
#5088=CIRCLE('',#12505,1.49999999999999);
#5089=CIRCLE('',#12506,1.49999999999999);
#5090=CIRCLE('',#12507,1.49999999999999);
#5091=CIRCLE('',#12508,1.49999999999999);
#5092=CIRCLE('',#12509,1.49999999999999);
#5093=CIRCLE('',#12510,1.49999999999999);
#5094=CIRCLE('',#12511,1.49999999999999);
#5095=CIRCLE('',#12512,1.49999999999999);
#5096=CIRCLE('',#12514,4.);
#5097=CIRCLE('',#12515,4.);
#5098=CIRCLE('',#12517,1.49999999999999);
#5099=CIRCLE('',#12518,1.49999999999999);
#5100=CIRCLE('',#12519,1.49999999999999);
#5101=CIRCLE('',#12520,1.49999999999999);
#5102=CIRCLE('',#12521,1.49999999999999);
#5103=CIRCLE('',#12522,1.49999999999999);
#5104=CIRCLE('',#12523,1.49999999999999);
#5105=CIRCLE('',#12524,1.49999999999999);
#5106=CIRCLE('',#12525,1.49999999999999);
#5107=CIRCLE('',#12526,1.49999999999999);
#5108=CIRCLE('',#12527,1.49999999999999);
#5109=CIRCLE('',#12545,1.49999999999999);
#5110=CIRCLE('',#12546,1.49999999999999);
#5111=CIRCLE('',#12547,1.49999999999999);
#5112=CIRCLE('',#12548,1.49999999999999);
#5113=CIRCLE('',#12549,1.49999999999999);
#5114=CIRCLE('',#12550,1.49999999999999);
#5115=CIRCLE('',#12551,1.49999999999999);
#5116=CIRCLE('',#12552,1.49999999999999);
#5117=CIRCLE('',#12553,1.49999999999999);
#5118=CIRCLE('',#12554,1.49999999999999);
#5119=CIRCLE('',#12555,1.49999999999999);
#5120=CIRCLE('',#12557,1.49999999999999);
#5121=CIRCLE('',#12559,1.49999999999999);
#5122=CIRCLE('',#12561,1.49999999999999);
#5123=CIRCLE('',#12563,1.49999999999999);
#5124=CIRCLE('',#12565,1.49999999999999);
#5125=CIRCLE('',#12567,1.49999999999999);
#5126=CIRCLE('',#12569,1.49999999999999);
#5127=CIRCLE('',#12571,1.49999999999999);
#5128=CIRCLE('',#12573,1.49999999999999);
#5129=CIRCLE('',#12575,1.49999999999999);
#5130=CIRCLE('',#12577,1.49999999999999);
#5961=VERTEX_POINT('',#18480);
#5962=VERTEX_POINT('',#18482);
#5963=VERTEX_POINT('',#18486);
#5964=VERTEX_POINT('',#18488);
#5965=VERTEX_POINT('',#18492);
#5966=VERTEX_POINT('',#18494);
#5967=VERTEX_POINT('',#18498);
#5968=VERTEX_POINT('',#18499);
#5969=VERTEX_POINT('',#18501);
#5970=VERTEX_POINT('',#18503);
#5971=VERTEX_POINT('',#18507);
#5972=VERTEX_POINT('',#18509);
#5973=VERTEX_POINT('',#18511);
#5974=VERTEX_POINT('',#18513);
#5975=VERTEX_POINT('',#18515);
#5976=VERTEX_POINT('',#18517);
#5977=VERTEX_POINT('',#18520);
#5978=VERTEX_POINT('',#18522);
#5979=VERTEX_POINT('',#18524);
#5980=VERTEX_POINT('',#18526);
#5981=VERTEX_POINT('',#18528);
#5982=VERTEX_POINT('',#18530);
#5983=VERTEX_POINT('',#18532);
#5984=VERTEX_POINT('',#18534);
#5985=VERTEX_POINT('',#18536);
#5986=VERTEX_POINT('',#18538);
#5987=VERTEX_POINT('',#18540);
#5988=VERTEX_POINT('',#18543);
#5989=VERTEX_POINT('',#18544);
#5990=VERTEX_POINT('',#18546);
#5991=VERTEX_POINT('',#18548);
#5992=VERTEX_POINT('',#18552);
#5993=VERTEX_POINT('',#18554);
#5994=VERTEX_POINT('',#18556);
#5995=VERTEX_POINT('',#18558);
#5996=VERTEX_POINT('',#18560);
#5997=VERTEX_POINT('',#18562);
#5998=VERTEX_POINT('',#18565);
#5999=VERTEX_POINT('',#18567);
#6000=VERTEX_POINT('',#18569);
#6001=VERTEX_POINT('',#18571);
#6002=VERTEX_POINT('',#18573);
#6003=VERTEX_POINT('',#18575);
#6004=VERTEX_POINT('',#18577);
#6005=VERTEX_POINT('',#18579);
#6006=VERTEX_POINT('',#18581);
#6007=VERTEX_POINT('',#18583);
#6008=VERTEX_POINT('',#18585);
#6009=VERTEX_POINT('',#18621);
#6010=VERTEX_POINT('',#18622);
#6011=VERTEX_POINT('',#18624);
#6012=VERTEX_POINT('',#18626);
#6013=VERTEX_POINT('',#18628);
#6014=VERTEX_POINT('',#18630);
#6015=VERTEX_POINT('',#18632);
#6016=VERTEX_POINT('',#18634);
#6017=VERTEX_POINT('',#18637);
#6018=VERTEX_POINT('',#18639);
#6019=VERTEX_POINT('',#18641);
#6020=VERTEX_POINT('',#18643);
#6021=VERTEX_POINT('',#18645);
#6022=VERTEX_POINT('',#18647);
#6023=VERTEX_POINT('',#18649);
#6024=VERTEX_POINT('',#18651);
#6025=VERTEX_POINT('',#18653);
#6026=VERTEX_POINT('',#18655);
#6027=VERTEX_POINT('',#18657);
#6028=VERTEX_POINT('',#18660);
#6029=VERTEX_POINT('',#18664);
#6030=VERTEX_POINT('',#18668);
#6031=VERTEX_POINT('',#18672);
#6032=VERTEX_POINT('',#18676);
#6033=VERTEX_POINT('',#18680);
#6034=VERTEX_POINT('',#18684);
#6035=VERTEX_POINT('',#18688);
#6036=VERTEX_POINT('',#18692);
#6037=VERTEX_POINT('',#18696);
#6038=VERTEX_POINT('',#18700);
#6039=VERTEX_POINT('',#18704);
#6040=VERTEX_POINT('',#18706);
#6041=VERTEX_POINT('',#18710);
#6042=VERTEX_POINT('',#18712);
#6043=VERTEX_POINT('',#18716);
#6044=VERTEX_POINT('',#18720);
#6045=VERTEX_POINT('',#18726);
#6046=VERTEX_POINT('',#18727);
#6047=VERTEX_POINT('',#18732);
#6048=VERTEX_POINT('',#18734);
#6049=VERTEX_POINT('',#18741);
#6050=VERTEX_POINT('',#18745);
#7373=EDGE_CURVE('',#5961,#5961,#5077,.T.);
#7374=EDGE_CURVE('',#5961,#5962,#1449,.T.);
#7375=EDGE_CURVE('',#5962,#5962,#5078,.T.);
#7376=EDGE_CURVE('',#5963,#5963,#5079,.T.);
#7377=EDGE_CURVE('',#5963,#5964,#1450,.T.);
#7378=EDGE_CURVE('',#5964,#5964,#5080,.T.);
#7379=EDGE_CURVE('',#5965,#5965,#5081,.T.);
#7380=EDGE_CURVE('',#5965,#5966,#1451,.T.);
#7381=EDGE_CURVE('',#5966,#5966,#5082,.T.);
#7382=EDGE_CURVE('',#5967,#5968,#5083,.T.);
#7383=EDGE_CURVE('',#5968,#5969,#1452,.T.);
#7384=EDGE_CURVE('',#5969,#5970,#5084,.T.);
#7385=EDGE_CURVE('',#5970,#5967,#1453,.T.);
#7386=EDGE_CURVE('',#5968,#5971,#1454,.T.);
#7387=EDGE_CURVE('',#5972,#5971,#1455,.T.);
#7388=EDGE_CURVE('',#5972,#5973,#1456,.T.);
#7389=EDGE_CURVE('',#5973,#5974,#1457,.T.);
#7390=EDGE_CURVE('',#5975,#5974,#1458,.T.);
#7391=EDGE_CURVE('',#5975,#5976,#1459,.T.);
#7392=EDGE_CURVE('',#5976,#5969,#1460,.T.);
#7393=EDGE_CURVE('',#5977,#5977,#5085,.T.);
#7394=EDGE_CURVE('',#5978,#5978,#5086,.T.);
#7395=EDGE_CURVE('',#5979,#5979,#5087,.T.);
#7396=EDGE_CURVE('',#5980,#5980,#5088,.T.);
#7397=EDGE_CURVE('',#5981,#5981,#5089,.T.);
#7398=EDGE_CURVE('',#5982,#5982,#5090,.T.);
#7399=EDGE_CURVE('',#5983,#5983,#5091,.T.);
#7400=EDGE_CURVE('',#5984,#5984,#5092,.T.);
#7401=EDGE_CURVE('',#5985,#5985,#5093,.T.);
#7402=EDGE_CURVE('',#5986,#5986,#5094,.T.);
#7403=EDGE_CURVE('',#5987,#5987,#5095,.T.);
#7404=EDGE_CURVE('',#5988,#5989,#5096,.T.);
#7405=EDGE_CURVE('',#5989,#5990,#1461,.T.);
#7406=EDGE_CURVE('',#5990,#5991,#5097,.T.);
#7407=EDGE_CURVE('',#5988,#5991,#1462,.T.);
#7408=EDGE_CURVE('',#5989,#5992,#1463,.T.);
#7409=EDGE_CURVE('',#5992,#5993,#1464,.T.);
#7410=EDGE_CURVE('',#5993,#5994,#1465,.T.);
#7411=EDGE_CURVE('',#5994,#5995,#1466,.T.);
#7412=EDGE_CURVE('',#5995,#5996,#1467,.T.);
#7413=EDGE_CURVE('',#5996,#5997,#1468,.T.);
#7414=EDGE_CURVE('',#5997,#5990,#1469,.T.);
#7415=EDGE_CURVE('',#5998,#5998,#5098,.T.);
#7416=EDGE_CURVE('',#5999,#5999,#5099,.T.);
#7417=EDGE_CURVE('',#6000,#6000,#5100,.T.);
#7418=EDGE_CURVE('',#6001,#6001,#5101,.T.);
#7419=EDGE_CURVE('',#6002,#6002,#5102,.T.);
#7420=EDGE_CURVE('',#6003,#6003,#5103,.T.);
#7421=EDGE_CURVE('',#6004,#6004,#5104,.T.);
#7422=EDGE_CURVE('',#6005,#6005,#5105,.T.);
#7423=EDGE_CURVE('',#6006,#6006,#5106,.T.);
#7424=EDGE_CURVE('',#6007,#6007,#5107,.T.);
#7425=EDGE_CURVE('',#6008,#6008,#5108,.T.);
#7426=EDGE_CURVE('',#5998,#5987,#1470,.T.);
#7427=EDGE_CURVE('',#5999,#5986,#1471,.T.);
#7428=EDGE_CURVE('',#6000,#5985,#1472,.T.);
#7429=EDGE_CURVE('',#6001,#5984,#1473,.T.);
#7430=EDGE_CURVE('',#6002,#5983,#1474,.T.);
#7431=EDGE_CURVE('',#6003,#5982,#1475,.T.);
#7432=EDGE_CURVE('',#6004,#5981,#1476,.T.);
#7433=EDGE_CURVE('',#6005,#5980,#1477,.T.);
#7434=EDGE_CURVE('',#6006,#5979,#1478,.T.);
#7435=EDGE_CURVE('',#6007,#5978,#1479,.T.);
#7436=EDGE_CURVE('',#6008,#5977,#1480,.T.);
#7437=EDGE_CURVE('',#5975,#5993,#1481,.T.);
#7438=EDGE_CURVE('',#5976,#5992,#1482,.T.);
#7439=EDGE_CURVE('',#5971,#5997,#1483,.T.);
#7440=EDGE_CURVE('',#5972,#5996,#1484,.T.);
#7441=EDGE_CURVE('',#5973,#5995,#1485,.T.);
#7442=EDGE_CURVE('',#5974,#5994,#1486,.T.);
#7443=EDGE_CURVE('',#6009,#6010,#1487,.T.);
#7444=EDGE_CURVE('',#6009,#6011,#1488,.T.);
#7445=EDGE_CURVE('',#6012,#6011,#1489,.T.);
#7446=EDGE_CURVE('',#6012,#6013,#1490,.T.);
#7447=EDGE_CURVE('',#6013,#6014,#1491,.T.);
#7448=EDGE_CURVE('',#6015,#6014,#1492,.T.);
#7449=EDGE_CURVE('',#6015,#6016,#1493,.T.);
#7450=EDGE_CURVE('',#6016,#6010,#1494,.T.);
#7451=EDGE_CURVE('',#6017,#6017,#5109,.T.);
#7452=EDGE_CURVE('',#6018,#6018,#5110,.T.);
#7453=EDGE_CURVE('',#6019,#6019,#5111,.T.);
#7454=EDGE_CURVE('',#6020,#6020,#5112,.T.);
#7455=EDGE_CURVE('',#6021,#6021,#5113,.T.);
#7456=EDGE_CURVE('',#6022,#6022,#5114,.T.);
#7457=EDGE_CURVE('',#6023,#6023,#5115,.T.);
#7458=EDGE_CURVE('',#6024,#6024,#5116,.T.);
#7459=EDGE_CURVE('',#6025,#6025,#5117,.T.);
#7460=EDGE_CURVE('',#6026,#6026,#5118,.T.);
#7461=EDGE_CURVE('',#6027,#6027,#5119,.T.);
#7462=EDGE_CURVE('',#6028,#6028,#5120,.T.);
#7463=EDGE_CURVE('',#6028,#6017,#1495,.T.);
#7464=EDGE_CURVE('',#6029,#6029,#5121,.T.);
#7465=EDGE_CURVE('',#6029,#6018,#1496,.T.);
#7466=EDGE_CURVE('',#6030,#6030,#5122,.T.);
#7467=EDGE_CURVE('',#6030,#6019,#1497,.T.);
#7468=EDGE_CURVE('',#6031,#6031,#5123,.T.);
#7469=EDGE_CURVE('',#6031,#6020,#1498,.T.);
#7470=EDGE_CURVE('',#6032,#6032,#5124,.T.);
#7471=EDGE_CURVE('',#6032,#6021,#1499,.T.);
#7472=EDGE_CURVE('',#6033,#6033,#5125,.T.);
#7473=EDGE_CURVE('',#6033,#6022,#1500,.T.);
#7474=EDGE_CURVE('',#6034,#6034,#5126,.T.);
#7475=EDGE_CURVE('',#6034,#6023,#1501,.T.);
#7476=EDGE_CURVE('',#6035,#6035,#5127,.T.);
#7477=EDGE_CURVE('',#6035,#6024,#1502,.T.);
#7478=EDGE_CURVE('',#6036,#6036,#5128,.T.);
#7479=EDGE_CURVE('',#6036,#6025,#1503,.T.);
#7480=EDGE_CURVE('',#6037,#6037,#5129,.T.);
#7481=EDGE_CURVE('',#6037,#6026,#1504,.T.);
#7482=EDGE_CURVE('',#6038,#6038,#5130,.T.);
#7483=EDGE_CURVE('',#6038,#6027,#1505,.T.);
#7484=EDGE_CURVE('',#6015,#6039,#1506,.T.);
#7485=EDGE_CURVE('',#6040,#6039,#1507,.T.);
#7486=EDGE_CURVE('',#6016,#6040,#1508,.T.);
#7487=EDGE_CURVE('',#6011,#6041,#1509,.T.);
#7488=EDGE_CURVE('',#6042,#6041,#1510,.T.);
#7489=EDGE_CURVE('',#6012,#6042,#1511,.T.);
#7490=EDGE_CURVE('',#6043,#6042,#1512,.T.);
#7491=EDGE_CURVE('',#6013,#6043,#1513,.T.);
#7492=EDGE_CURVE('',#6044,#6043,#1514,.T.);
#7493=EDGE_CURVE('',#6014,#6044,#1515,.T.);
#7494=EDGE_CURVE('',#6039,#6044,#1516,.T.);
#7495=EDGE_CURVE('',#6045,#6046,#1517,.T.);
#7496=EDGE_CURVE('',#6045,#6040,#1518,.T.);
#7497=EDGE_CURVE('',#6041,#6046,#1519,.T.);
#7498=EDGE_CURVE('',#5988,#6047,#1520,.T.);
#7499=EDGE_CURVE('',#5991,#6048,#1521,.T.);
#7500=EDGE_CURVE('',#6047,#6048,#1522,.T.);
#7501=EDGE_CURVE('',#5970,#6045,#1523,.T.);
#7502=EDGE_CURVE('',#5967,#6046,#1524,.T.);
#7503=EDGE_CURVE('',#6049,#6047,#1525,.T.);
#7504=EDGE_CURVE('',#6010,#6049,#1526,.T.);
#7505=EDGE_CURVE('',#6050,#6049,#1527,.T.);
#7506=EDGE_CURVE('',#6009,#6050,#1528,.T.);
#7507=EDGE_CURVE('',#6048,#6050,#1529,.T.);
#10084=ORIENTED_EDGE('',*,*,#7373,.F.);
#10085=ORIENTED_EDGE('',*,*,#7374,.T.);
#10086=ORIENTED_EDGE('',*,*,#7375,.F.);
#10087=ORIENTED_EDGE('',*,*,#7374,.F.);
#10088=ORIENTED_EDGE('',*,*,#7376,.F.);
#10089=ORIENTED_EDGE('',*,*,#7377,.T.);
#10090=ORIENTED_EDGE('',*,*,#7378,.F.);
#10091=ORIENTED_EDGE('',*,*,#7377,.F.);
#10092=ORIENTED_EDGE('',*,*,#7379,.F.);
#10093=ORIENTED_EDGE('',*,*,#7380,.T.);
#10094=ORIENTED_EDGE('',*,*,#7381,.F.);
#10095=ORIENTED_EDGE('',*,*,#7380,.F.);
#10096=ORIENTED_EDGE('',*,*,#7382,.T.);
#10097=ORIENTED_EDGE('',*,*,#7383,.T.);
#10098=ORIENTED_EDGE('',*,*,#7384,.T.);
#10099=ORIENTED_EDGE('',*,*,#7385,.T.);
#10100=ORIENTED_EDGE('',*,*,#7383,.F.);
#10101=ORIENTED_EDGE('',*,*,#7386,.T.);
#10102=ORIENTED_EDGE('',*,*,#7387,.F.);
#10103=ORIENTED_EDGE('',*,*,#7388,.T.);
#10104=ORIENTED_EDGE('',*,*,#7389,.T.);
#10105=ORIENTED_EDGE('',*,*,#7390,.F.);
#10106=ORIENTED_EDGE('',*,*,#7391,.T.);
#10107=ORIENTED_EDGE('',*,*,#7392,.T.);
#10108=ORIENTED_EDGE('',*,*,#7393,.F.);
#10109=ORIENTED_EDGE('',*,*,#7394,.F.);
#10110=ORIENTED_EDGE('',*,*,#7395,.F.);
#10111=ORIENTED_EDGE('',*,*,#7396,.F.);
#10112=ORIENTED_EDGE('',*,*,#7397,.F.);
#10113=ORIENTED_EDGE('',*,*,#7398,.F.);
#10114=ORIENTED_EDGE('',*,*,#7399,.F.);
#10115=ORIENTED_EDGE('',*,*,#7400,.F.);
#10116=ORIENTED_EDGE('',*,*,#7401,.F.);
#10117=ORIENTED_EDGE('',*,*,#7402,.F.);
#10118=ORIENTED_EDGE('',*,*,#7403,.F.);
#10119=ORIENTED_EDGE('',*,*,#7404,.T.);
#10120=ORIENTED_EDGE('',*,*,#7405,.T.);
#10121=ORIENTED_EDGE('',*,*,#7406,.T.);
#10122=ORIENTED_EDGE('',*,*,#7407,.F.);
#10123=ORIENTED_EDGE('',*,*,#7405,.F.);
#10124=ORIENTED_EDGE('',*,*,#7408,.T.);
#10125=ORIENTED_EDGE('',*,*,#7409,.T.);
#10126=ORIENTED_EDGE('',*,*,#7410,.T.);
#10127=ORIENTED_EDGE('',*,*,#7411,.T.);
#10128=ORIENTED_EDGE('',*,*,#7412,.T.);
#10129=ORIENTED_EDGE('',*,*,#7413,.T.);
#10130=ORIENTED_EDGE('',*,*,#7414,.T.);
#10131=ORIENTED_EDGE('',*,*,#7415,.T.);
#10132=ORIENTED_EDGE('',*,*,#7416,.T.);
#10133=ORIENTED_EDGE('',*,*,#7417,.T.);
#10134=ORIENTED_EDGE('',*,*,#7418,.T.);
#10135=ORIENTED_EDGE('',*,*,#7419,.T.);
#10136=ORIENTED_EDGE('',*,*,#7420,.T.);
#10137=ORIENTED_EDGE('',*,*,#7421,.T.);
#10138=ORIENTED_EDGE('',*,*,#7422,.T.);
#10139=ORIENTED_EDGE('',*,*,#7423,.T.);
#10140=ORIENTED_EDGE('',*,*,#7424,.T.);
#10141=ORIENTED_EDGE('',*,*,#7425,.T.);
#10142=ORIENTED_EDGE('',*,*,#7415,.F.);
#10143=ORIENTED_EDGE('',*,*,#7426,.T.);
#10144=ORIENTED_EDGE('',*,*,#7403,.T.);
#10145=ORIENTED_EDGE('',*,*,#7426,.F.);
#10146=ORIENTED_EDGE('',*,*,#7416,.F.);
#10147=ORIENTED_EDGE('',*,*,#7427,.T.);
#10148=ORIENTED_EDGE('',*,*,#7402,.T.);
#10149=ORIENTED_EDGE('',*,*,#7427,.F.);
#10150=ORIENTED_EDGE('',*,*,#7417,.F.);
#10151=ORIENTED_EDGE('',*,*,#7428,.T.);
#10152=ORIENTED_EDGE('',*,*,#7401,.T.);
#10153=ORIENTED_EDGE('',*,*,#7428,.F.);
#10154=ORIENTED_EDGE('',*,*,#7418,.F.);
#10155=ORIENTED_EDGE('',*,*,#7429,.T.);
#10156=ORIENTED_EDGE('',*,*,#7400,.T.);
#10157=ORIENTED_EDGE('',*,*,#7429,.F.);
#10158=ORIENTED_EDGE('',*,*,#7419,.F.);
#10159=ORIENTED_EDGE('',*,*,#7430,.T.);
#10160=ORIENTED_EDGE('',*,*,#7399,.T.);
#10161=ORIENTED_EDGE('',*,*,#7430,.F.);
#10162=ORIENTED_EDGE('',*,*,#7420,.F.);
#10163=ORIENTED_EDGE('',*,*,#7431,.T.);
#10164=ORIENTED_EDGE('',*,*,#7398,.T.);
#10165=ORIENTED_EDGE('',*,*,#7431,.F.);
#10166=ORIENTED_EDGE('',*,*,#7421,.F.);
#10167=ORIENTED_EDGE('',*,*,#7432,.T.);
#10168=ORIENTED_EDGE('',*,*,#7397,.T.);
#10169=ORIENTED_EDGE('',*,*,#7432,.F.);
#10170=ORIENTED_EDGE('',*,*,#7422,.F.);
#10171=ORIENTED_EDGE('',*,*,#7433,.T.);
#10172=ORIENTED_EDGE('',*,*,#7396,.T.);
#10173=ORIENTED_EDGE('',*,*,#7433,.F.);
#10174=ORIENTED_EDGE('',*,*,#7423,.F.);
#10175=ORIENTED_EDGE('',*,*,#7434,.T.);
#10176=ORIENTED_EDGE('',*,*,#7395,.T.);
#10177=ORIENTED_EDGE('',*,*,#7434,.F.);
#10178=ORIENTED_EDGE('',*,*,#7424,.F.);
#10179=ORIENTED_EDGE('',*,*,#7435,.T.);
#10180=ORIENTED_EDGE('',*,*,#7394,.T.);
#10181=ORIENTED_EDGE('',*,*,#7435,.F.);
#10182=ORIENTED_EDGE('',*,*,#7425,.F.);
#10183=ORIENTED_EDGE('',*,*,#7436,.T.);
#10184=ORIENTED_EDGE('',*,*,#7393,.T.);
#10185=ORIENTED_EDGE('',*,*,#7436,.F.);
#10186=ORIENTED_EDGE('',*,*,#7391,.F.);
#10187=ORIENTED_EDGE('',*,*,#7437,.T.);
#10188=ORIENTED_EDGE('',*,*,#7409,.F.);
#10189=ORIENTED_EDGE('',*,*,#7438,.F.);
#10190=ORIENTED_EDGE('',*,*,#7387,.T.);
#10191=ORIENTED_EDGE('',*,*,#7439,.T.);
#10192=ORIENTED_EDGE('',*,*,#7413,.F.);
#10193=ORIENTED_EDGE('',*,*,#7440,.F.);
#10194=ORIENTED_EDGE('',*,*,#7388,.F.);
#10195=ORIENTED_EDGE('',*,*,#7440,.T.);
#10196=ORIENTED_EDGE('',*,*,#7412,.F.);
#10197=ORIENTED_EDGE('',*,*,#7441,.F.);
#10198=ORIENTED_EDGE('',*,*,#7389,.F.);
#10199=ORIENTED_EDGE('',*,*,#7441,.T.);
#10200=ORIENTED_EDGE('',*,*,#7411,.F.);
#10201=ORIENTED_EDGE('',*,*,#7442,.F.);
#10202=ORIENTED_EDGE('',*,*,#7390,.T.);
#10203=ORIENTED_EDGE('',*,*,#7442,.T.);
#10204=ORIENTED_EDGE('',*,*,#7410,.F.);
#10205=ORIENTED_EDGE('',*,*,#7437,.F.);
#10206=ORIENTED_EDGE('',*,*,#7443,.F.);
#10207=ORIENTED_EDGE('',*,*,#7444,.T.);
#10208=ORIENTED_EDGE('',*,*,#7445,.F.);
#10209=ORIENTED_EDGE('',*,*,#7446,.T.);
#10210=ORIENTED_EDGE('',*,*,#7447,.T.);
#10211=ORIENTED_EDGE('',*,*,#7448,.F.);
#10212=ORIENTED_EDGE('',*,*,#7449,.T.);
#10213=ORIENTED_EDGE('',*,*,#7450,.T.);
#10214=ORIENTED_EDGE('',*,*,#7451,.F.);
#10215=ORIENTED_EDGE('',*,*,#7452,.F.);
#10216=ORIENTED_EDGE('',*,*,#7453,.F.);
#10217=ORIENTED_EDGE('',*,*,#7454,.F.);
#10218=ORIENTED_EDGE('',*,*,#7455,.F.);
#10219=ORIENTED_EDGE('',*,*,#7456,.F.);
#10220=ORIENTED_EDGE('',*,*,#7457,.F.);
#10221=ORIENTED_EDGE('',*,*,#7458,.F.);
#10222=ORIENTED_EDGE('',*,*,#7459,.F.);
#10223=ORIENTED_EDGE('',*,*,#7460,.F.);
#10224=ORIENTED_EDGE('',*,*,#7461,.F.);
#10225=ORIENTED_EDGE('',*,*,#7462,.F.);
#10226=ORIENTED_EDGE('',*,*,#7463,.T.);
#10227=ORIENTED_EDGE('',*,*,#7451,.T.);
#10228=ORIENTED_EDGE('',*,*,#7463,.F.);
#10229=ORIENTED_EDGE('',*,*,#7464,.F.);
#10230=ORIENTED_EDGE('',*,*,#7465,.T.);
#10231=ORIENTED_EDGE('',*,*,#7452,.T.);
#10232=ORIENTED_EDGE('',*,*,#7465,.F.);
#10233=ORIENTED_EDGE('',*,*,#7466,.F.);
#10234=ORIENTED_EDGE('',*,*,#7467,.T.);
#10235=ORIENTED_EDGE('',*,*,#7453,.T.);
#10236=ORIENTED_EDGE('',*,*,#7467,.F.);
#10237=ORIENTED_EDGE('',*,*,#7468,.F.);
#10238=ORIENTED_EDGE('',*,*,#7469,.T.);
#10239=ORIENTED_EDGE('',*,*,#7454,.T.);
#10240=ORIENTED_EDGE('',*,*,#7469,.F.);
#10241=ORIENTED_EDGE('',*,*,#7470,.F.);
#10242=ORIENTED_EDGE('',*,*,#7471,.T.);
#10243=ORIENTED_EDGE('',*,*,#7455,.T.);
#10244=ORIENTED_EDGE('',*,*,#7471,.F.);
#10245=ORIENTED_EDGE('',*,*,#7472,.F.);
#10246=ORIENTED_EDGE('',*,*,#7473,.T.);
#10247=ORIENTED_EDGE('',*,*,#7456,.T.);
#10248=ORIENTED_EDGE('',*,*,#7473,.F.);
#10249=ORIENTED_EDGE('',*,*,#7474,.F.);
#10250=ORIENTED_EDGE('',*,*,#7475,.T.);
#10251=ORIENTED_EDGE('',*,*,#7457,.T.);
#10252=ORIENTED_EDGE('',*,*,#7475,.F.);
#10253=ORIENTED_EDGE('',*,*,#7476,.F.);
#10254=ORIENTED_EDGE('',*,*,#7477,.T.);
#10255=ORIENTED_EDGE('',*,*,#7458,.T.);
#10256=ORIENTED_EDGE('',*,*,#7477,.F.);
#10257=ORIENTED_EDGE('',*,*,#7478,.F.);
#10258=ORIENTED_EDGE('',*,*,#7479,.T.);
#10259=ORIENTED_EDGE('',*,*,#7459,.T.);
#10260=ORIENTED_EDGE('',*,*,#7479,.F.);
#10261=ORIENTED_EDGE('',*,*,#7480,.F.);
#10262=ORIENTED_EDGE('',*,*,#7481,.T.);
#10263=ORIENTED_EDGE('',*,*,#7460,.T.);
#10264=ORIENTED_EDGE('',*,*,#7481,.F.);
#10265=ORIENTED_EDGE('',*,*,#7482,.F.);
#10266=ORIENTED_EDGE('',*,*,#7483,.T.);
#10267=ORIENTED_EDGE('',*,*,#7461,.T.);
#10268=ORIENTED_EDGE('',*,*,#7483,.F.);
#10269=ORIENTED_EDGE('',*,*,#7449,.F.);
#10270=ORIENTED_EDGE('',*,*,#7484,.T.);
#10271=ORIENTED_EDGE('',*,*,#7485,.F.);
#10272=ORIENTED_EDGE('',*,*,#7486,.F.);
#10273=ORIENTED_EDGE('',*,*,#7445,.T.);
#10274=ORIENTED_EDGE('',*,*,#7487,.T.);
#10275=ORIENTED_EDGE('',*,*,#7488,.F.);
#10276=ORIENTED_EDGE('',*,*,#7489,.F.);
#10277=ORIENTED_EDGE('',*,*,#7446,.F.);
#10278=ORIENTED_EDGE('',*,*,#7489,.T.);
#10279=ORIENTED_EDGE('',*,*,#7490,.F.);
#10280=ORIENTED_EDGE('',*,*,#7491,.F.);
#10281=ORIENTED_EDGE('',*,*,#7447,.F.);
#10282=ORIENTED_EDGE('',*,*,#7491,.T.);
#10283=ORIENTED_EDGE('',*,*,#7492,.F.);
#10284=ORIENTED_EDGE('',*,*,#7493,.F.);
#10285=ORIENTED_EDGE('',*,*,#7448,.T.);
#10286=ORIENTED_EDGE('',*,*,#7493,.T.);
#10287=ORIENTED_EDGE('',*,*,#7494,.F.);
#10288=ORIENTED_EDGE('',*,*,#7484,.F.);
#10289=ORIENTED_EDGE('',*,*,#7495,.F.);
#10290=ORIENTED_EDGE('',*,*,#7496,.T.);
#10291=ORIENTED_EDGE('',*,*,#7485,.T.);
#10292=ORIENTED_EDGE('',*,*,#7494,.T.);
#10293=ORIENTED_EDGE('',*,*,#7492,.T.);
#10294=ORIENTED_EDGE('',*,*,#7490,.T.);
#10295=ORIENTED_EDGE('',*,*,#7488,.T.);
#10296=ORIENTED_EDGE('',*,*,#7497,.T.);
#10297=ORIENTED_EDGE('',*,*,#7462,.T.);
#10298=ORIENTED_EDGE('',*,*,#7464,.T.);
#10299=ORIENTED_EDGE('',*,*,#7466,.T.);
#10300=ORIENTED_EDGE('',*,*,#7468,.T.);
#10301=ORIENTED_EDGE('',*,*,#7470,.T.);
#10302=ORIENTED_EDGE('',*,*,#7472,.T.);
#10303=ORIENTED_EDGE('',*,*,#7474,.T.);
#10304=ORIENTED_EDGE('',*,*,#7476,.T.);
#10305=ORIENTED_EDGE('',*,*,#7478,.T.);
#10306=ORIENTED_EDGE('',*,*,#7480,.T.);
#10307=ORIENTED_EDGE('',*,*,#7482,.T.);
#10308=ORIENTED_EDGE('',*,*,#7498,.F.);
#10309=ORIENTED_EDGE('',*,*,#7407,.T.);
#10310=ORIENTED_EDGE('',*,*,#7499,.T.);
#10311=ORIENTED_EDGE('',*,*,#7500,.F.);
#10312=ORIENTED_EDGE('',*,*,#7375,.T.);
#10313=ORIENTED_EDGE('',*,*,#7376,.T.);
#10314=ORIENTED_EDGE('',*,*,#7379,.T.);
#10315=ORIENTED_EDGE('',*,*,#7385,.F.);
#10316=ORIENTED_EDGE('',*,*,#7501,.T.);
#10317=ORIENTED_EDGE('',*,*,#7495,.T.);
#10318=ORIENTED_EDGE('',*,*,#7502,.F.);
#10319=ORIENTED_EDGE('',*,*,#7373,.T.);
#10320=ORIENTED_EDGE('',*,*,#7498,.T.);
#10321=ORIENTED_EDGE('',*,*,#7503,.F.);
#10322=ORIENTED_EDGE('',*,*,#7504,.F.);
#10323=ORIENTED_EDGE('',*,*,#7450,.F.);
#10324=ORIENTED_EDGE('',*,*,#7486,.T.);
#10325=ORIENTED_EDGE('',*,*,#7496,.F.);
#10326=ORIENTED_EDGE('',*,*,#7501,.F.);
#10327=ORIENTED_EDGE('',*,*,#7384,.F.);
#10328=ORIENTED_EDGE('',*,*,#7392,.F.);
#10329=ORIENTED_EDGE('',*,*,#7438,.T.);
#10330=ORIENTED_EDGE('',*,*,#7408,.F.);
#10331=ORIENTED_EDGE('',*,*,#7404,.F.);
#10332=ORIENTED_EDGE('',*,*,#7443,.T.);
#10333=ORIENTED_EDGE('',*,*,#7504,.T.);
#10334=ORIENTED_EDGE('',*,*,#7505,.F.);
#10335=ORIENTED_EDGE('',*,*,#7506,.F.);
#10336=ORIENTED_EDGE('',*,*,#7378,.T.);
#10337=ORIENTED_EDGE('',*,*,#7381,.T.);
#10338=ORIENTED_EDGE('',*,*,#7499,.F.);
#10339=ORIENTED_EDGE('',*,*,#7406,.F.);
#10340=ORIENTED_EDGE('',*,*,#7414,.F.);
#10341=ORIENTED_EDGE('',*,*,#7439,.F.);
#10342=ORIENTED_EDGE('',*,*,#7386,.F.);
#10343=ORIENTED_EDGE('',*,*,#7382,.F.);
#10344=ORIENTED_EDGE('',*,*,#7502,.T.);
#10345=ORIENTED_EDGE('',*,*,#7497,.F.);
#10346=ORIENTED_EDGE('',*,*,#7487,.F.);
#10347=ORIENTED_EDGE('',*,*,#7444,.F.);
#10348=ORIENTED_EDGE('',*,*,#7506,.T.);
#10349=ORIENTED_EDGE('',*,*,#7507,.F.);
#10350=ORIENTED_EDGE('',*,*,#7500,.T.);
#10351=ORIENTED_EDGE('',*,*,#7507,.T.);
#10352=ORIENTED_EDGE('',*,*,#7505,.T.);
#10353=ORIENTED_EDGE('',*,*,#7503,.T.);
#11188=ADVANCED_FACE('',(#3312),#2829,.F.);
#11189=ADVANCED_FACE('',(#3313),#2830,.F.);
#11190=ADVANCED_FACE('',(#3314),#2831,.F.);
#11191=ADVANCED_FACE('',(#3315),#2832,.F.);
#11192=ADVANCED_FACE('',(#3316,#567,#568,#569,#570,#571,#572,#573,#574,
#575,#576,#577),#760,.F.);
#11193=ADVANCED_FACE('',(#3317),#2833,.T.);
#11194=ADVANCED_FACE('',(#3318,#578,#579,#580,#581,#582,#583,#584,#585,
#586,#587,#588),#761,.T.);
#11195=ADVANCED_FACE('',(#3319),#2834,.F.);
#11196=ADVANCED_FACE('',(#3320),#2835,.F.);
#11197=ADVANCED_FACE('',(#3321),#2836,.F.);
#11198=ADVANCED_FACE('',(#3322),#2837,.F.);
#11199=ADVANCED_FACE('',(#3323),#2838,.F.);
#11200=ADVANCED_FACE('',(#3324),#2839,.F.);
#11201=ADVANCED_FACE('',(#3325),#2840,.F.);
#11202=ADVANCED_FACE('',(#3326),#2841,.F.);
#11203=ADVANCED_FACE('',(#3327),#2842,.F.);
#11204=ADVANCED_FACE('',(#3328),#2843,.F.);
#11205=ADVANCED_FACE('',(#3329),#2844,.F.);
#11206=ADVANCED_FACE('',(#3330),#762,.T.);
#11207=ADVANCED_FACE('',(#3331),#763,.T.);
#11208=ADVANCED_FACE('',(#3332),#764,.T.);
#11209=ADVANCED_FACE('',(#3333),#765,.T.);
#11210=ADVANCED_FACE('',(#3334),#766,.T.);
#11211=ADVANCED_FACE('',(#3335,#589,#590,#591,#592,#593,#594,#595,#596,
#597,#598,#599),#767,.F.);
#11212=ADVANCED_FACE('',(#3336),#2845,.F.);
#11213=ADVANCED_FACE('',(#3337),#2846,.F.);
#11214=ADVANCED_FACE('',(#3338),#2847,.F.);
#11215=ADVANCED_FACE('',(#3339),#2848,.F.);
#11216=ADVANCED_FACE('',(#3340),#2849,.F.);
#11217=ADVANCED_FACE('',(#3341),#2850,.F.);
#11218=ADVANCED_FACE('',(#3342),#2851,.F.);
#11219=ADVANCED_FACE('',(#3343),#2852,.F.);
#11220=ADVANCED_FACE('',(#3344),#2853,.F.);
#11221=ADVANCED_FACE('',(#3345),#2854,.F.);
#11222=ADVANCED_FACE('',(#3346),#2855,.F.);
#11223=ADVANCED_FACE('',(#3347),#768,.T.);
#11224=ADVANCED_FACE('',(#3348),#769,.T.);
#11225=ADVANCED_FACE('',(#3349),#770,.T.);
#11226=ADVANCED_FACE('',(#3350),#771,.T.);
#11227=ADVANCED_FACE('',(#3351),#772,.T.);
#11228=ADVANCED_FACE('',(#3352,#600,#601,#602,#603,#604,#605,#606,#607,
#608,#609,#610),#773,.T.);
#11229=ADVANCED_FACE('',(#3353,#611,#612,#613),#774,.T.);
#11230=ADVANCED_FACE('',(#3354,#614),#775,.T.);
#11231=ADVANCED_FACE('',(#3355),#776,.T.);
#11232=ADVANCED_FACE('',(#3356,#615,#616),#777,.T.);
#11233=ADVANCED_FACE('',(#3357),#778,.T.);
#11234=ADVANCED_FACE('',(#3358),#779,.T.);
#11322=CLOSED_SHELL('',(#11188,#11189,#11190,#11191,#11192,#11193,#11194,
#11195,#11196,#11197,#11198,#11199,#11200,#11201,#11202,#11203,#11204,#11205,
#11206,#11207,#11208,#11209,#11210,#11211,#11212,#11213,#11214,#11215,#11216,
#11217,#11218,#11219,#11220,#11221,#11222,#11223,#11224,#11225,#11226,#11227,
#11228,#11229,#11230,#11231,#11232,#11233,#11234));
#12488=AXIS2_PLACEMENT_3D('',#18478,#15348,#15349);
#12489=AXIS2_PLACEMENT_3D('',#18479,#15350,#15351);
#12490=AXIS2_PLACEMENT_3D('',#18481,#15352,#15353);
#12491=AXIS2_PLACEMENT_3D('',#18484,#15355,#15356);
#12492=AXIS2_PLACEMENT_3D('',#18485,#15357,#15358);
#12493=AXIS2_PLACEMENT_3D('',#18487,#15359,#15360);
#12494=AXIS2_PLACEMENT_3D('',#18490,#15362,#15363);
#12495=AXIS2_PLACEMENT_3D('',#18491,#15364,#15365);
#12496=AXIS2_PLACEMENT_3D('',#18493,#15366,#15367);
#12497=AXIS2_PLACEMENT_3D('',#18496,#15369,#15370);
#12498=AXIS2_PLACEMENT_3D('',#18497,#15371,#15372);
#12499=AXIS2_PLACEMENT_3D('',#18500,#15373,#15374);
#12500=AXIS2_PLACEMENT_3D('',#18504,#15376,#15377);
#12501=AXIS2_PLACEMENT_3D('',#18506,#15379,#15380);
#12502=AXIS2_PLACEMENT_3D('',#18521,#15388,#15389);
#12503=AXIS2_PLACEMENT_3D('',#18523,#15390,#15391);
#12504=AXIS2_PLACEMENT_3D('',#18525,#15392,#15393);
#12505=AXIS2_PLACEMENT_3D('',#18527,#15394,#15395);
#12506=AXIS2_PLACEMENT_3D('',#18529,#15396,#15397);
#12507=AXIS2_PLACEMENT_3D('',#18531,#15398,#15399);
#12508=AXIS2_PLACEMENT_3D('',#18533,#15400,#15401);
#12509=AXIS2_PLACEMENT_3D('',#18535,#15402,#15403);
#12510=AXIS2_PLACEMENT_3D('',#18537,#15404,#15405);
#12511=AXIS2_PLACEMENT_3D('',#18539,#15406,#15407);
#12512=AXIS2_PLACEMENT_3D('',#18541,#15408,#15409);
#12513=AXIS2_PLACEMENT_3D('',#18542,#15410,#15411);
#12514=AXIS2_PLACEMENT_3D('',#18545,#15412,#15413);
#12515=AXIS2_PLACEMENT_3D('',#18549,#15415,#15416);
#12516=AXIS2_PLACEMENT_3D('',#18551,#15418,#15419);
#12517=AXIS2_PLACEMENT_3D('',#18566,#15427,#15428);
#12518=AXIS2_PLACEMENT_3D('',#18568,#15429,#15430);
#12519=AXIS2_PLACEMENT_3D('',#18570,#15431,#15432);
#12520=AXIS2_PLACEMENT_3D('',#18572,#15433,#15434);
#12521=AXIS2_PLACEMENT_3D('',#18574,#15435,#15436);
#12522=AXIS2_PLACEMENT_3D('',#18576,#15437,#15438);
#12523=AXIS2_PLACEMENT_3D('',#18578,#15439,#15440);
#12524=AXIS2_PLACEMENT_3D('',#18580,#15441,#15442);
#12525=AXIS2_PLACEMENT_3D('',#18582,#15443,#15444);
#12526=AXIS2_PLACEMENT_3D('',#18584,#15445,#15446);
#12527=AXIS2_PLACEMENT_3D('',#18586,#15447,#15448);
#12528=AXIS2_PLACEMENT_3D('',#18587,#15449,#15450);
#12529=AXIS2_PLACEMENT_3D('',#18589,#15452,#15453);
#12530=AXIS2_PLACEMENT_3D('',#18591,#15455,#15456);
#12531=AXIS2_PLACEMENT_3D('',#18593,#15458,#15459);
#12532=AXIS2_PLACEMENT_3D('',#18595,#15461,#15462);
#12533=AXIS2_PLACEMENT_3D('',#18597,#15464,#15465);
#12534=AXIS2_PLACEMENT_3D('',#18599,#15467,#15468);
#12535=AXIS2_PLACEMENT_3D('',#18601,#15470,#15471);
#12536=AXIS2_PLACEMENT_3D('',#18603,#15473,#15474);
#12537=AXIS2_PLACEMENT_3D('',#18605,#15476,#15477);
#12538=AXIS2_PLACEMENT_3D('',#18607,#15479,#15480);
#12539=AXIS2_PLACEMENT_3D('',#18609,#15482,#15483);
#12540=AXIS2_PLACEMENT_3D('',#18612,#15486,#15487);
#12541=AXIS2_PLACEMENT_3D('',#18615,#15490,#15491);
#12542=AXIS2_PLACEMENT_3D('',#18617,#15493,#15494);
#12543=AXIS2_PLACEMENT_3D('',#18619,#15496,#15497);
#12544=AXIS2_PLACEMENT_3D('',#18620,#15498,#15499);
#12545=AXIS2_PLACEMENT_3D('',#18638,#15508,#15509);
#12546=AXIS2_PLACEMENT_3D('',#18640,#15510,#15511);
#12547=AXIS2_PLACEMENT_3D('',#18642,#15512,#15513);
#12548=AXIS2_PLACEMENT_3D('',#18644,#15514,#15515);
#12549=AXIS2_PLACEMENT_3D('',#18646,#15516,#15517);
#12550=AXIS2_PLACEMENT_3D('',#18648,#15518,#15519);
#12551=AXIS2_PLACEMENT_3D('',#18650,#15520,#15521);
#12552=AXIS2_PLACEMENT_3D('',#18652,#15522,#15523);
#12553=AXIS2_PLACEMENT_3D('',#18654,#15524,#15525);
#12554=AXIS2_PLACEMENT_3D('',#18656,#15526,#15527);
#12555=AXIS2_PLACEMENT_3D('',#18658,#15528,#15529);
#12556=AXIS2_PLACEMENT_3D('',#18659,#15530,#15531);
#12557=AXIS2_PLACEMENT_3D('',#18661,#15532,#15533);
#12558=AXIS2_PLACEMENT_3D('',#18663,#15535,#15536);
#12559=AXIS2_PLACEMENT_3D('',#18665,#15537,#15538);
#12560=AXIS2_PLACEMENT_3D('',#18667,#15540,#15541);
#12561=AXIS2_PLACEMENT_3D('',#18669,#15542,#15543);
#12562=AXIS2_PLACEMENT_3D('',#18671,#15545,#15546);
#12563=AXIS2_PLACEMENT_3D('',#18673,#15547,#15548);
#12564=AXIS2_PLACEMENT_3D('',#18675,#15550,#15551);
#12565=AXIS2_PLACEMENT_3D('',#18677,#15552,#15553);
#12566=AXIS2_PLACEMENT_3D('',#18679,#15555,#15556);
#12567=AXIS2_PLACEMENT_3D('',#18681,#15557,#15558);
#12568=AXIS2_PLACEMENT_3D('',#18683,#15560,#15561);
#12569=AXIS2_PLACEMENT_3D('',#18685,#15562,#15563);
#12570=AXIS2_PLACEMENT_3D('',#18687,#15565,#15566);
#12571=AXIS2_PLACEMENT_3D('',#18689,#15567,#15568);
#12572=AXIS2_PLACEMENT_3D('',#18691,#15570,#15571);
#12573=AXIS2_PLACEMENT_3D('',#18693,#15572,#15573);
#12574=AXIS2_PLACEMENT_3D('',#18695,#15575,#15576);
#12575=AXIS2_PLACEMENT_3D('',#18697,#15577,#15578);
#12576=AXIS2_PLACEMENT_3D('',#18699,#15580,#15581);
#12577=AXIS2_PLACEMENT_3D('',#18701,#15582,#15583);
#12578=AXIS2_PLACEMENT_3D('',#18703,#15585,#15586);
#12579=AXIS2_PLACEMENT_3D('',#18709,#15590,#15591);
#12580=AXIS2_PLACEMENT_3D('',#18715,#15595,#15596);
#12581=AXIS2_PLACEMENT_3D('',#18719,#15599,#15600);
#12582=AXIS2_PLACEMENT_3D('',#18723,#15603,#15604);
#12583=AXIS2_PLACEMENT_3D('',#18725,#15606,#15607);
#12584=AXIS2_PLACEMENT_3D('',#18731,#15611,#15612);
#12585=AXIS2_PLACEMENT_3D('',#18737,#15616,#15617);
#12586=AXIS2_PLACEMENT_3D('',#18740,#15620,#15621);
#12587=AXIS2_PLACEMENT_3D('',#18744,#15624,#15625);
#12588=AXIS2_PLACEMENT_3D('',#18748,#15628,#15629);
#12589=AXIS2_PLACEMENT_3D('',#18750,#15631,#15632);
#15348=DIRECTION('axis',(0.,0.,1.));
#15349=DIRECTION('refdir',(1.,0.,0.));
#15350=DIRECTION('center_axis',(0.,1.,0.));
#15351=DIRECTION('ref_axis',(1.,0.,0.));
#15352=DIRECTION('center_axis',(0.,1.,0.));
#15353=DIRECTION('ref_axis',(1.,0.,0.));
#15354=DIRECTION('',(0.,1.,0.));
#15355=DIRECTION('center_axis',(0.,-1.,0.));
#15356=DIRECTION('ref_axis',(1.,0.,0.));
#15357=DIRECTION('center_axis',(0.,-1.,0.));
#15358=DIRECTION('ref_axis',(-1.,0.,0.));
#15359=DIRECTION('center_axis',(0.,-1.,0.));
#15360=DIRECTION('ref_axis',(-1.,0.,0.));
#15361=DIRECTION('',(0.,-1.,0.));
#15362=DIRECTION('center_axis',(0.,1.,0.));
#15363=DIRECTION('ref_axis',(-1.,0.,0.));
#15364=DIRECTION('center_axis',(0.,-1.,0.));
#15365=DIRECTION('ref_axis',(-1.,0.,0.));
#15366=DIRECTION('center_axis',(0.,-1.,0.));
#15367=DIRECTION('ref_axis',(-1.,0.,0.));
#15368=DIRECTION('',(0.,-1.,0.));
#15369=DIRECTION('center_axis',(0.,1.,0.));
#15370=DIRECTION('ref_axis',(-1.,0.,0.));
#15371=DIRECTION('center_axis',(-1.,0.,0.));
#15372=DIRECTION('ref_axis',(0.,0.707106781186546,0.707106781186549));
#15373=DIRECTION('center_axis',(1.,0.,0.));
#15374=DIRECTION('ref_axis',(0.,0.707106781186546,0.707106781186549));
#15375=DIRECTION('',(-1.,0.,0.));
#15376=DIRECTION('center_axis',(-1.,0.,0.));
#15377=DIRECTION('ref_axis',(0.,0.707106781186546,0.707106781186549));
#15378=DIRECTION('',(1.,0.,0.));
#15379=DIRECTION('center_axis',(0.,0.,1.));
#15380=DIRECTION('ref_axis',(1.,0.,0.));
#15381=DIRECTION('',(0.,-1.,0.));
#15382=DIRECTION('',(-0.707106781186546,0.707106781186549,0.));
#15383=DIRECTION('',(-0.707106781186546,-0.707106781186549,0.));
#15384=DIRECTION('',(-1.,0.,0.));
#15385=DIRECTION('',(0.707106781186546,-0.707106781186549,0.));
#15386=DIRECTION('',(0.707106781186546,0.707106781186549,0.));
#15387=DIRECTION('',(0.,1.,0.));
#15388=DIRECTION('center_axis',(0.,0.,-1.));
#15389=DIRECTION('ref_axis',(1.,0.,0.));
#15390=DIRECTION('center_axis',(0.,0.,-1.));
#15391=DIRECTION('ref_axis',(1.,0.,0.));
#15392=DIRECTION('center_axis',(0.,0.,-1.));
#15393=DIRECTION('ref_axis',(1.,0.,0.));
#15394=DIRECTION('center_axis',(0.,0.,-1.));
#15395=DIRECTION('ref_axis',(1.,0.,0.));
#15396=DIRECTION('center_axis',(0.,0.,-1.));
#15397=DIRECTION('ref_axis',(1.,0.,0.));
#15398=DIRECTION('center_axis',(0.,0.,-1.));
#15399=DIRECTION('ref_axis',(1.,0.,0.));
#15400=DIRECTION('center_axis',(0.,0.,-1.));
#15401=DIRECTION('ref_axis',(1.,0.,0.));
#15402=DIRECTION('center_axis',(0.,0.,-1.));
#15403=DIRECTION('ref_axis',(1.,0.,0.));
#15404=DIRECTION('center_axis',(0.,0.,-1.));
#15405=DIRECTION('ref_axis',(1.,0.,0.));
#15406=DIRECTION('center_axis',(0.,0.,-1.));
#15407=DIRECTION('ref_axis',(1.,0.,0.));
#15408=DIRECTION('center_axis',(0.,0.,-1.));
#15409=DIRECTION('ref_axis',(1.,0.,0.));
#15410=DIRECTION('center_axis',(1.,0.,0.));
#15411=DIRECTION('ref_axis',(0.,0.992156741649222,0.125));
#15412=DIRECTION('center_axis',(1.,0.,0.));
#15413=DIRECTION('ref_axis',(0.,0.992156741649222,0.125));
#15414=DIRECTION('',(1.,0.,0.));
#15415=DIRECTION('center_axis',(-1.,0.,0.));
#15416=DIRECTION('ref_axis',(0.,0.992156741649222,0.125));
#15417=DIRECTION('',(1.,0.,0.));
#15418=DIRECTION('center_axis',(0.,0.,1.));
#15419=DIRECTION('ref_axis',(1.,0.,0.));
#15420=DIRECTION('',(0.,-1.,0.));
#15421=DIRECTION('',(-0.707106781186546,-0.707106781186549,0.));
#15422=DIRECTION('',(0.707106781186546,-0.707106781186549,0.));
#15423=DIRECTION('',(1.,0.,0.));
#15424=DIRECTION('',(0.707106781186546,0.707106781186549,0.));
#15425=DIRECTION('',(-0.707106781186546,0.707106781186549,0.));
#15426=DIRECTION('',(0.,1.,0.));
#15427=DIRECTION('center_axis',(0.,0.,-1.));
#15428=DIRECTION('ref_axis',(1.,0.,0.));
#15429=DIRECTION('center_axis',(0.,0.,-1.));
#15430=DIRECTION('ref_axis',(1.,0.,0.));
#15431=DIRECTION('center_axis',(0.,0.,-1.));
#15432=DIRECTION('ref_axis',(1.,0.,0.));
#15433=DIRECTION('center_axis',(0.,0.,-1.));
#15434=DIRECTION('ref_axis',(1.,0.,0.));
#15435=DIRECTION('center_axis',(0.,0.,-1.));
#15436=DIRECTION('ref_axis',(1.,0.,0.));
#15437=DIRECTION('center_axis',(0.,0.,-1.));
#15438=DIRECTION('ref_axis',(1.,0.,0.));
#15439=DIRECTION('center_axis',(0.,0.,-1.));
#15440=DIRECTION('ref_axis',(1.,0.,0.));
#15441=DIRECTION('center_axis',(0.,0.,-1.));
#15442=DIRECTION('ref_axis',(1.,0.,0.));
#15443=DIRECTION('center_axis',(0.,0.,-1.));
#15444=DIRECTION('ref_axis',(1.,0.,0.));
#15445=DIRECTION('center_axis',(0.,0.,-1.));
#15446=DIRECTION('ref_axis',(1.,0.,0.));
#15447=DIRECTION('center_axis',(0.,0.,-1.));
#15448=DIRECTION('ref_axis',(1.,0.,0.));
#15449=DIRECTION('center_axis',(0.,0.,1.));
#15450=DIRECTION('ref_axis',(1.,0.,0.));
#15451=DIRECTION('',(0.,0.,-1.));
#15452=DIRECTION('center_axis',(0.,0.,1.));
#15453=DIRECTION('ref_axis',(1.,0.,0.));
#15454=DIRECTION('',(0.,0.,-1.));
#15455=DIRECTION('center_axis',(0.,0.,1.));
#15456=DIRECTION('ref_axis',(1.,0.,0.));
#15457=DIRECTION('',(0.,0.,-1.));
#15458=DIRECTION('center_axis',(0.,0.,1.));
#15459=DIRECTION('ref_axis',(1.,0.,0.));
#15460=DIRECTION('',(0.,0.,-1.));
#15461=DIRECTION('center_axis',(0.,0.,1.));
#15462=DIRECTION('ref_axis',(1.,0.,0.));
#15463=DIRECTION('',(0.,0.,-1.));
#15464=DIRECTION('center_axis',(0.,0.,1.));
#15465=DIRECTION('ref_axis',(1.,0.,0.));
#15466=DIRECTION('',(0.,0.,-1.));
#15467=DIRECTION('center_axis',(0.,0.,1.));
#15468=DIRECTION('ref_axis',(1.,0.,0.));
#15469=DIRECTION('',(0.,0.,-1.));
#15470=DIRECTION('center_axis',(0.,0.,1.));
#15471=DIRECTION('ref_axis',(1.,0.,0.));
#15472=DIRECTION('',(0.,0.,-1.));
#15473=DIRECTION('center_axis',(0.,0.,1.));
#15474=DIRECTION('ref_axis',(1.,0.,0.));
#15475=DIRECTION('',(0.,0.,-1.));
#15476=DIRECTION('center_axis',(0.,0.,1.));
#15477=DIRECTION('ref_axis',(1.,0.,0.));
#15478=DIRECTION('',(0.,0.,-1.));
#15479=DIRECTION('center_axis',(0.,0.,1.));
#15480=DIRECTION('ref_axis',(1.,0.,0.));
#15481=DIRECTION('',(0.,0.,-1.));
#15482=DIRECTION('center_axis',(-0.707106781186549,0.707106781186546,0.));
#15483=DIRECTION('ref_axis',(-0.707106781186546,-0.707106781186549,0.));
#15484=DIRECTION('',(0.,0.,1.));
#15485=DIRECTION('',(0.,0.,1.));
#15486=DIRECTION('center_axis',(0.707106781186549,0.707106781186546,0.));
#15487=DIRECTION('ref_axis',(-0.707106781186546,0.707106781186549,0.));
#15488=DIRECTION('',(0.,0.,1.));
#15489=DIRECTION('',(0.,0.,1.));
#15490=DIRECTION('center_axis',(0.707106781186549,-0.707106781186546,0.));
#15491=DIRECTION('ref_axis',(0.707106781186546,0.707106781186549,0.));
#15492=DIRECTION('',(0.,0.,1.));
#15493=DIRECTION('center_axis',(0.,-1.,0.));
#15494=DIRECTION('ref_axis',(1.,0.,0.));
#15495=DIRECTION('',(0.,0.,1.));
#15496=DIRECTION('center_axis',(-0.707106781186549,-0.707106781186546,0.));
#15497=DIRECTION('ref_axis',(0.707106781186546,-0.707106781186549,0.));
#15498=DIRECTION('center_axis',(0.,0.,1.));
#15499=DIRECTION('ref_axis',(1.,0.,0.));
#15500=DIRECTION('',(-1.,0.,0.));
#15501=DIRECTION('',(0.,-1.,0.));
#15502=DIRECTION('',(-0.707106781186546,0.707106781186549,0.));
#15503=DIRECTION('',(-0.707106781186546,-0.707106781186549,0.));
#15504=DIRECTION('',(-1.,0.,0.));
#15505=DIRECTION('',(0.707106781186546,-0.707106781186549,0.));
#15506=DIRECTION('',(0.707106781186546,0.707106781186549,0.));
#15507=DIRECTION('',(0.,1.,0.));
#15508=DIRECTION('center_axis',(0.,0.,-1.));
#15509=DIRECTION('ref_axis',(1.,0.,0.));
#15510=DIRECTION('center_axis',(0.,0.,-1.));
#15511=DIRECTION('ref_axis',(1.,0.,0.));
#15512=DIRECTION('center_axis',(0.,0.,-1.));
#15513=DIRECTION('ref_axis',(1.,0.,0.));
#15514=DIRECTION('center_axis',(0.,0.,-1.));
#15515=DIRECTION('ref_axis',(1.,0.,0.));
#15516=DIRECTION('center_axis',(0.,0.,-1.));
#15517=DIRECTION('ref_axis',(1.,0.,0.));
#15518=DIRECTION('center_axis',(0.,0.,-1.));
#15519=DIRECTION('ref_axis',(1.,0.,0.));
#15520=DIRECTION('center_axis',(0.,0.,-1.));
#15521=DIRECTION('ref_axis',(1.,0.,0.));
#15522=DIRECTION('center_axis',(0.,0.,-1.));
#15523=DIRECTION('ref_axis',(1.,0.,0.));
#15524=DIRECTION('center_axis',(0.,0.,-1.));
#15525=DIRECTION('ref_axis',(1.,0.,0.));
#15526=DIRECTION('center_axis',(0.,0.,-1.));
#15527=DIRECTION('ref_axis',(1.,0.,0.));
#15528=DIRECTION('center_axis',(0.,0.,-1.));
#15529=DIRECTION('ref_axis',(1.,0.,0.));
#15530=DIRECTION('center_axis',(0.,0.,1.));
#15531=DIRECTION('ref_axis',(1.,0.,0.));
#15532=DIRECTION('center_axis',(0.,0.,-1.));
#15533=DIRECTION('ref_axis',(1.,0.,0.));
#15534=DIRECTION('',(0.,0.,-1.));
#15535=DIRECTION('center_axis',(0.,0.,1.));
#15536=DIRECTION('ref_axis',(1.,0.,0.));
#15537=DIRECTION('center_axis',(0.,0.,-1.));
#15538=DIRECTION('ref_axis',(1.,0.,0.));
#15539=DIRECTION('',(0.,0.,-1.));
#15540=DIRECTION('center_axis',(0.,0.,1.));
#15541=DIRECTION('ref_axis',(1.,0.,0.));
#15542=DIRECTION('center_axis',(0.,0.,-1.));
#15543=DIRECTION('ref_axis',(1.,0.,0.));
#15544=DIRECTION('',(0.,0.,-1.));
#15545=DIRECTION('center_axis',(0.,0.,1.));
#15546=DIRECTION('ref_axis',(1.,0.,0.));
#15547=DIRECTION('center_axis',(0.,0.,-1.));
#15548=DIRECTION('ref_axis',(1.,0.,0.));
#15549=DIRECTION('',(0.,0.,-1.));
#15550=DIRECTION('center_axis',(0.,0.,1.));
#15551=DIRECTION('ref_axis',(1.,0.,0.));
#15552=DIRECTION('center_axis',(0.,0.,-1.));
#15553=DIRECTION('ref_axis',(1.,0.,0.));
#15554=DIRECTION('',(0.,0.,-1.));
#15555=DIRECTION('center_axis',(0.,0.,1.));
#15556=DIRECTION('ref_axis',(1.,0.,0.));
#15557=DIRECTION('center_axis',(0.,0.,-1.));
#15558=DIRECTION('ref_axis',(1.,0.,0.));
#15559=DIRECTION('',(0.,0.,-1.));
#15560=DIRECTION('center_axis',(0.,0.,1.));
#15561=DIRECTION('ref_axis',(1.,0.,0.));
#15562=DIRECTION('center_axis',(0.,0.,-1.));
#15563=DIRECTION('ref_axis',(1.,0.,0.));
#15564=DIRECTION('',(0.,0.,-1.));
#15565=DIRECTION('center_axis',(0.,0.,1.));
#15566=DIRECTION('ref_axis',(1.,0.,0.));
#15567=DIRECTION('center_axis',(0.,0.,-1.));
#15568=DIRECTION('ref_axis',(1.,0.,0.));
#15569=DIRECTION('',(0.,0.,-1.));
#15570=DIRECTION('center_axis',(0.,0.,1.));
#15571=DIRECTION('ref_axis',(1.,0.,0.));
#15572=DIRECTION('center_axis',(0.,0.,-1.));
#15573=DIRECTION('ref_axis',(1.,0.,0.));
#15574=DIRECTION('',(0.,0.,-1.));
#15575=DIRECTION('center_axis',(0.,0.,1.));
#15576=DIRECTION('ref_axis',(1.,0.,0.));
#15577=DIRECTION('center_axis',(0.,0.,-1.));
#15578=DIRECTION('ref_axis',(1.,0.,0.));
#15579=DIRECTION('',(0.,0.,-1.));
#15580=DIRECTION('center_axis',(0.,0.,1.));
#15581=DIRECTION('ref_axis',(1.,0.,0.));
#15582=DIRECTION('center_axis',(0.,0.,-1.));
#15583=DIRECTION('ref_axis',(1.,0.,0.));
#15584=DIRECTION('',(0.,0.,-1.));
#15585=DIRECTION('center_axis',(-0.707106781186549,0.707106781186546,0.));
#15586=DIRECTION('ref_axis',(-0.707106781186546,-0.707106781186549,0.));
#15587=DIRECTION('',(0.,0.,1.));
#15588=DIRECTION('',(-0.707106781186546,-0.707106781186549,0.));
#15589=DIRECTION('',(0.,0.,1.));
#15590=DIRECTION('center_axis',(0.707106781186549,0.707106781186546,0.));
#15591=DIRECTION('ref_axis',(-0.707106781186546,0.707106781186549,0.));
#15592=DIRECTION('',(0.,0.,1.));
#15593=DIRECTION('',(-0.707106781186546,0.707106781186549,0.));
#15594=DIRECTION('',(0.,0.,1.));
#15595=DIRECTION('center_axis',(0.707106781186549,-0.707106781186546,0.));
#15596=DIRECTION('ref_axis',(0.707106781186546,0.707106781186549,0.));
#15597=DIRECTION('',(0.707106781186546,0.707106781186549,0.));
#15598=DIRECTION('',(0.,0.,1.));
#15599=DIRECTION('center_axis',(0.,-1.,0.));
#15600=DIRECTION('ref_axis',(1.,0.,0.));
#15601=DIRECTION('',(1.,0.,0.));
#15602=DIRECTION('',(0.,0.,1.));
#15603=DIRECTION('center_axis',(-0.707106781186549,-0.707106781186546,0.));
#15604=DIRECTION('ref_axis',(0.707106781186546,-0.707106781186549,0.));
#15605=DIRECTION('',(0.707106781186546,-0.707106781186549,0.));
#15606=DIRECTION('center_axis',(0.,0.,1.));
#15607=DIRECTION('ref_axis',(1.,0.,0.));
#15608=DIRECTION('',(1.,0.,0.));
#15609=DIRECTION('',(0.,-1.,0.));
#15610=DIRECTION('',(0.,1.,0.));
#15611=DIRECTION('center_axis',(0.,1.,0.));
#15612=DIRECTION('ref_axis',(1.,0.,0.));
#15613=DIRECTION('',(0.,0.,-1.));
#15614=DIRECTION('',(0.,0.,-1.));
#15615=DIRECTION('',(1.,0.,0.));
#15616=DIRECTION('center_axis',(0.,-1.,0.));
#15617=DIRECTION('ref_axis',(-1.,0.,0.));
#15618=DIRECTION('',(0.,0.,-1.));
#15619=DIRECTION('',(0.,0.,-1.));
#15620=DIRECTION('center_axis',(-1.,0.,0.));
#15621=DIRECTION('ref_axis',(0.,1.,0.));
#15622=DIRECTION('',(0.,1.,0.));
#15623=DIRECTION('',(0.,0.,-1.));
#15624=DIRECTION('center_axis',(0.,-1.,0.));
#15625=DIRECTION('ref_axis',(-1.,0.,0.));
#15626=DIRECTION('',(-1.,0.,0.));
#15627=DIRECTION('',(0.,0.,-1.));
#15628=DIRECTION('center_axis',(1.,0.,0.));
#15629=DIRECTION('ref_axis',(0.,-1.,0.));
#15630=DIRECTION('',(0.,-1.,0.));
#15631=DIRECTION('center_axis',(0.,0.,-1.));
#15632=DIRECTION('ref_axis',(-1.,0.,0.));
#18478=CARTESIAN_POINT('',(0.,0.,0.));
#18479=CARTESIAN_POINT('Origin',(67.9877341799264,50.,25.7372649179816));
#18480=CARTESIAN_POINT('',(66.4877341799264,50.,25.7372649179816));
#18481=CARTESIAN_POINT('Origin',(67.9877341799264,50.,25.7372649179816));
#18482=CARTESIAN_POINT('',(66.4877341799264,53.,25.7372649179816));
#18483=CARTESIAN_POINT('',(66.4877341799264,50.,25.7372649179816));
#18484=CARTESIAN_POINT('Origin',(67.9877341799264,53.,25.7372649179816));
#18485=CARTESIAN_POINT('Origin',(72.0217856971541,53.,3.89451831659521));
#18486=CARTESIAN_POINT('',(74.0217856971541,53.,3.89451831659521));
#18487=CARTESIAN_POINT('Origin',(72.0217856971541,53.,3.89451831659521));
#18488=CARTESIAN_POINT('',(74.0217856971541,50.,3.89451831659521));
#18489=CARTESIAN_POINT('',(74.0217856971541,53.,3.89451831659521));
#18490=CARTESIAN_POINT('Origin',(72.0217856971541,50.,3.89451831659521));
#18491=CARTESIAN_POINT('Origin',(64.0217856971541,53.,3.89451831659521));
#18492=CARTESIAN_POINT('',(66.0217856971541,53.,3.89451831659521));
#18493=CARTESIAN_POINT('Origin',(64.0217856971541,53.,3.89451831659521));
#18494=CARTESIAN_POINT('',(66.0217856971541,50.,3.89451831659521));
#18495=CARTESIAN_POINT('',(66.0217856971541,53.,3.89451831659521));
#18496=CARTESIAN_POINT('Origin',(64.0217856971541,50.,3.89451831659521));
#18497=CARTESIAN_POINT('Origin',(71.9522002739937,48.,28.4747649179816));
#18498=CARTESIAN_POINT('',(75.916666368061,50.,28.4747649179816));
#18499=CARTESIAN_POINT('',(75.916666368061,48.,30.4747649179816));
#18500=CARTESIAN_POINT('Origin',(75.916666368061,48.,28.4747649179816));
#18501=CARTESIAN_POINT('',(60.0588019917919,48.,30.4747649179816));
#18502=CARTESIAN_POINT('',(71.9522002739937,48.,30.4747649179816));
#18503=CARTESIAN_POINT('',(60.0588019917919,50.,28.4747649179816));
#18504=CARTESIAN_POINT('Origin',(60.0588019917919,48.,28.4747649179816));
#18505=CARTESIAN_POINT('',(71.9522002739937,50.,28.4747649179816));
#18506=CARTESIAN_POINT('Origin',(67.9877341799264,35.4644660940673,30.4747649179816));
#18507=CARTESIAN_POINT('',(75.916666368061,32.0710678118655,30.4747649179816));
#18508=CARTESIAN_POINT('',(75.916666368061,50.,30.4747649179816));
#18509=CARTESIAN_POINT('',(82.9877341799264,25.,30.4747649179816));
#18510=CARTESIAN_POINT('',(82.9877341799264,25.,30.4747649179816));
#18511=CARTESIAN_POINT('',(75.916666368061,17.9289321881345,30.4747649179816));
#18512=CARTESIAN_POINT('',(82.9877341799264,25.,30.4747649179816));
#18513=CARTESIAN_POINT('',(60.0588019917919,17.9289321881345,30.4747649179816));
#18514=CARTESIAN_POINT('',(75.916666368061,17.9289321881345,30.4747649179816));
#18515=CARTESIAN_POINT('',(52.9877341799264,25.,30.4747649179816));
#18516=CARTESIAN_POINT('',(52.9877341799264,25.,30.4747649179816));
#18517=CARTESIAN_POINT('',(60.0588019917919,32.0710678118655,30.4747649179816));
#18518=CARTESIAN_POINT('',(52.9877341799264,25.,30.4747649179816));
#18519=CARTESIAN_POINT('',(60.0588019917919,50.,30.4747649179816));
#18520=CARTESIAN_POINT('',(66.3814154642151,29.,30.4747649179816));
#18521=CARTESIAN_POINT('Origin',(67.8814154642151,29.,30.4747649179816));
#18522=CARTESIAN_POINT('',(57.131415464215,25.,30.4747649179816));
#18523=CARTESIAN_POINT('Origin',(58.631415464215,25.,30.4747649179816));
#18524=CARTESIAN_POINT('',(71.0064154642151,21.,30.4747649179816));
#18525=CARTESIAN_POINT('Origin',(72.5064154642151,21.,30.4747649179816));
#18526=CARTESIAN_POINT('',(61.756415464215,21.,30.4747649179816));
#18527=CARTESIAN_POINT('Origin',(63.256415464215,21.,30.4747649179816));
#18528=CARTESIAN_POINT('',(66.3814154642151,25.,30.4747649179816));
#18529=CARTESIAN_POINT('Origin',(67.8814154642151,25.,30.4747649179816));
#18530=CARTESIAN_POINT('',(66.3814154642151,21.,30.4747649179816));
#18531=CARTESIAN_POINT('Origin',(67.8814154642151,21.,30.4747649179816));
#18532=CARTESIAN_POINT('',(71.0064154642151,25.,30.4747649179816));
#18533=CARTESIAN_POINT('Origin',(72.5064154642151,25.,30.4747649179816));
#18534=CARTESIAN_POINT('',(61.756415464215,25.,30.4747649179816));
#18535=CARTESIAN_POINT('Origin',(63.256415464215,25.,30.4747649179816));
#18536=CARTESIAN_POINT('',(61.756415464215,29.,30.4747649179816));
#18537=CARTESIAN_POINT('Origin',(63.256415464215,29.,30.4747649179816));
#18538=CARTESIAN_POINT('',(71.0064154642151,29.,30.4747649179816));
#18539=CARTESIAN_POINT('Origin',(72.5064154642151,29.,30.4747649179816));
#18540=CARTESIAN_POINT('',(75.6314154642151,25.,30.4747649179816));
#18541=CARTESIAN_POINT('Origin',(77.131415464215,25.,30.4747649179816));
#18542=CARTESIAN_POINT('Origin',(60.0588019917919,49.0313730334031,29.9747649179816));
#18543=CARTESIAN_POINT('',(60.0588019917919,53.,30.4747649179816));
#18544=CARTESIAN_POINT('',(60.0588019917919,49.0313730334031,33.9747649179816));
#18545=CARTESIAN_POINT('Origin',(60.0588019917919,49.0313730334031,29.9747649179816));
#18546=CARTESIAN_POINT('',(75.916666368061,49.0313730334031,33.9747649179816));
#18547=CARTESIAN_POINT('',(60.0588019917919,49.0313730334031,33.9747649179816));
#18548=CARTESIAN_POINT('',(75.916666368061,53.,30.4747649179816));
#18549=CARTESIAN_POINT('Origin',(75.916666368061,49.0313730334031,29.9747649179816));
#18550=CARTESIAN_POINT('',(60.0588019917919,53.,30.4747649179816));
#18551=CARTESIAN_POINT('Origin',(67.9877341799264,35.4644660940673,33.9747649179816));
#18552=CARTESIAN_POINT('',(60.0588019917919,32.0710678118655,33.9747649179816));
#18553=CARTESIAN_POINT('',(60.0588019917919,50.,33.9747649179816));
#18554=CARTESIAN_POINT('',(52.9877341799264,25.,33.9747649179816));
#18555=CARTESIAN_POINT('',(52.9877341799264,25.,33.9747649179816));
#18556=CARTESIAN_POINT('',(60.0588019917919,17.9289321881345,33.9747649179816));
#18557=CARTESIAN_POINT('',(52.9877341799264,25.,33.9747649179816));
#18558=CARTESIAN_POINT('',(75.916666368061,17.9289321881345,33.9747649179816));
#18559=CARTESIAN_POINT('',(75.916666368061,17.9289321881345,33.9747649179816));
#18560=CARTESIAN_POINT('',(82.9877341799264,25.,33.9747649179816));
#18561=CARTESIAN_POINT('',(82.9877341799264,25.,33.9747649179816));
#18562=CARTESIAN_POINT('',(75.916666368061,32.0710678118655,33.9747649179816));
#18563=CARTESIAN_POINT('',(82.9877341799264,25.,33.9747649179816));
#18564=CARTESIAN_POINT('',(75.916666368061,50.,33.9747649179816));
#18565=CARTESIAN_POINT('',(75.6314154642151,25.,33.9747649179816));
#18566=CARTESIAN_POINT('Origin',(77.131415464215,25.,33.9747649179816));
#18567=CARTESIAN_POINT('',(71.0064154642151,29.,33.9747649179816));
#18568=CARTESIAN_POINT('Origin',(72.5064154642151,29.,33.9747649179816));
#18569=CARTESIAN_POINT('',(61.756415464215,29.,33.9747649179816));
#18570=CARTESIAN_POINT('Origin',(63.256415464215,29.,33.9747649179816));
#18571=CARTESIAN_POINT('',(61.756415464215,25.,33.9747649179816));
#18572=CARTESIAN_POINT('Origin',(63.256415464215,25.,33.9747649179816));
#18573=CARTESIAN_POINT('',(71.0064154642151,25.,33.9747649179816));
#18574=CARTESIAN_POINT('Origin',(72.5064154642151,25.,33.9747649179816));
#18575=CARTESIAN_POINT('',(66.3814154642151,21.,33.9747649179816));
#18576=CARTESIAN_POINT('Origin',(67.8814154642151,21.,33.9747649179816));
#18577=CARTESIAN_POINT('',(66.3814154642151,25.,33.9747649179816));
#18578=CARTESIAN_POINT('Origin',(67.8814154642151,25.,33.9747649179816));
#18579=CARTESIAN_POINT('',(61.756415464215,21.,33.9747649179816));
#18580=CARTESIAN_POINT('Origin',(63.256415464215,21.,33.9747649179816));
#18581=CARTESIAN_POINT('',(71.0064154642151,21.,33.9747649179816));
#18582=CARTESIAN_POINT('Origin',(72.5064154642151,21.,33.9747649179816));
#18583=CARTESIAN_POINT('',(57.131415464215,25.,33.9747649179816));
#18584=CARTESIAN_POINT('Origin',(58.631415464215,25.,33.9747649179816));
#18585=CARTESIAN_POINT('',(66.3814154642151,29.,33.9747649179816));
#18586=CARTESIAN_POINT('Origin',(67.8814154642151,29.,33.9747649179816));
#18587=CARTESIAN_POINT('Origin',(77.131415464215,25.,30.4747649179816));
#18588=CARTESIAN_POINT('',(75.6314154642151,25.,30.4747649179816));
#18589=CARTESIAN_POINT('Origin',(72.5064154642151,29.,30.4747649179816));
#18590=CARTESIAN_POINT('',(71.0064154642151,29.,30.4747649179816));
#18591=CARTESIAN_POINT('Origin',(63.256415464215,29.,30.4747649179816));
#18592=CARTESIAN_POINT('',(61.756415464215,29.,30.4747649179816));
#18593=CARTESIAN_POINT('Origin',(63.256415464215,25.,30.4747649179816));
#18594=CARTESIAN_POINT('',(61.756415464215,25.,30.4747649179816));
#18595=CARTESIAN_POINT('Origin',(72.5064154642151,25.,30.4747649179816));
#18596=CARTESIAN_POINT('',(71.0064154642151,25.,30.4747649179816));
#18597=CARTESIAN_POINT('Origin',(67.8814154642151,21.,30.4747649179816));
#18598=CARTESIAN_POINT('',(66.3814154642151,21.,30.4747649179816));
#18599=CARTESIAN_POINT('Origin',(67.8814154642151,25.,30.4747649179816));
#18600=CARTESIAN_POINT('',(66.3814154642151,25.,30.4747649179816));
#18601=CARTESIAN_POINT('Origin',(63.256415464215,21.,30.4747649179816));
#18602=CARTESIAN_POINT('',(61.756415464215,21.,30.4747649179816));
#18603=CARTESIAN_POINT('Origin',(72.5064154642151,21.,30.4747649179816));
#18604=CARTESIAN_POINT('',(71.0064154642151,21.,30.4747649179816));
#18605=CARTESIAN_POINT('Origin',(58.631415464215,25.,30.4747649179816));
#18606=CARTESIAN_POINT('',(57.131415464215,25.,30.4747649179816));
#18607=CARTESIAN_POINT('Origin',(67.8814154642151,29.,30.4747649179816));
#18608=CARTESIAN_POINT('',(66.3814154642151,29.,30.4747649179816));
#18609=CARTESIAN_POINT('Origin',(60.0588019917919,32.0710678118655,30.4747649179816));
#18610=CARTESIAN_POINT('',(52.9877341799264,25.,30.4747649179816));
#18611=CARTESIAN_POINT('',(60.0588019917919,32.0710678118655,30.4747649179816));
#18612=CARTESIAN_POINT('Origin',(82.9877341799264,25.,30.4747649179816));
#18613=CARTESIAN_POINT('',(75.916666368061,32.0710678118655,30.4747649179816));
#18614=CARTESIAN_POINT('',(82.9877341799264,25.,30.4747649179816));
#18615=CARTESIAN_POINT('Origin',(75.916666368061,17.9289321881345,30.4747649179816));
#18616=CARTESIAN_POINT('',(75.916666368061,17.9289321881345,30.4747649179816));
#18617=CARTESIAN_POINT('Origin',(60.0588019917919,17.9289321881345,30.4747649179816));
#18618=CARTESIAN_POINT('',(60.0588019917919,17.9289321881345,30.4747649179816));
#18619=CARTESIAN_POINT('Origin',(52.9877341799264,25.,30.4747649179816));
#18620=CARTESIAN_POINT('Origin',(67.9877341799264,35.4644660940673,19.4747649179816));
#18621=CARTESIAN_POINT('',(75.916666368061,50.,19.4747649179816));
#18622=CARTESIAN_POINT('',(60.0588019917919,50.,19.4747649179816));
#18623=CARTESIAN_POINT('',(71.9522002739937,50.,19.4747649179816));
#18624=CARTESIAN_POINT('',(75.916666368061,32.0710678118655,19.4747649179816));
#18625=CARTESIAN_POINT('',(75.916666368061,50.,19.4747649179816));
#18626=CARTESIAN_POINT('',(82.9877341799264,25.,19.4747649179816));
#18627=CARTESIAN_POINT('',(82.9877341799264,25.,19.4747649179816));
#18628=CARTESIAN_POINT('',(75.916666368061,17.9289321881345,19.4747649179816));
#18629=CARTESIAN_POINT('',(82.9877341799264,25.,19.4747649179816));
#18630=CARTESIAN_POINT('',(60.0588019917919,17.9289321881345,19.4747649179816));
#18631=CARTESIAN_POINT('',(75.916666368061,17.9289321881345,19.4747649179816));
#18632=CARTESIAN_POINT('',(52.9877341799264,25.,19.4747649179816));
#18633=CARTESIAN_POINT('',(52.9877341799264,25.,19.4747649179816));
#18634=CARTESIAN_POINT('',(60.0588019917919,32.0710678118655,19.4747649179816));
#18635=CARTESIAN_POINT('',(52.9877341799264,25.,19.4747649179816));
#18636=CARTESIAN_POINT('',(60.0588019917919,50.,19.4747649179816));
#18637=CARTESIAN_POINT('',(75.6314154642151,25.,19.4747649179816));
#18638=CARTESIAN_POINT('Origin',(77.131415464215,25.,19.4747649179816));
#18639=CARTESIAN_POINT('',(71.0064154642151,29.,19.4747649179816));
#18640=CARTESIAN_POINT('Origin',(72.5064154642151,29.,19.4747649179816));
#18641=CARTESIAN_POINT('',(61.756415464215,29.,19.4747649179816));
#18642=CARTESIAN_POINT('Origin',(63.256415464215,29.,19.4747649179816));
#18643=CARTESIAN_POINT('',(61.756415464215,25.,19.4747649179816));
#18644=CARTESIAN_POINT('Origin',(63.256415464215,25.,19.4747649179816));
#18645=CARTESIAN_POINT('',(71.0064154642151,25.,19.4747649179816));
#18646=CARTESIAN_POINT('Origin',(72.5064154642151,25.,19.4747649179816));
#18647=CARTESIAN_POINT('',(66.3814154642151,21.,19.4747649179816));
#18648=CARTESIAN_POINT('Origin',(67.8814154642151,21.,19.4747649179816));
#18649=CARTESIAN_POINT('',(66.3814154642151,25.,19.4747649179816));
#18650=CARTESIAN_POINT('Origin',(67.8814154642151,25.,19.4747649179816));
#18651=CARTESIAN_POINT('',(61.756415464215,21.,19.4747649179816));
#18652=CARTESIAN_POINT('Origin',(63.256415464215,21.,19.4747649179816));
#18653=CARTESIAN_POINT('',(71.0064154642151,21.,19.4747649179816));
#18654=CARTESIAN_POINT('Origin',(72.5064154642151,21.,19.4747649179816));
#18655=CARTESIAN_POINT('',(57.131415464215,25.,19.4747649179816));
#18656=CARTESIAN_POINT('Origin',(58.631415464215,25.,19.4747649179816));
#18657=CARTESIAN_POINT('',(66.3814154642151,29.,19.4747649179816));
#18658=CARTESIAN_POINT('Origin',(67.8814154642151,29.,19.4747649179816));
#18659=CARTESIAN_POINT('Origin',(77.131415464215,25.,19.4747649179816));
#18660=CARTESIAN_POINT('',(75.6314154642151,25.,22.9997649179816));
#18661=CARTESIAN_POINT('Origin',(77.131415464215,25.,22.9997649179816));
#18662=CARTESIAN_POINT('',(75.6314154642151,25.,19.4747649179816));
#18663=CARTESIAN_POINT('Origin',(72.5064154642151,29.,19.4747649179816));
#18664=CARTESIAN_POINT('',(71.0064154642151,29.,22.9997649179816));
#18665=CARTESIAN_POINT('Origin',(72.5064154642151,29.,22.9997649179816));
#18666=CARTESIAN_POINT('',(71.0064154642151,29.,19.4747649179816));
#18667=CARTESIAN_POINT('Origin',(63.256415464215,29.,19.4747649179816));
#18668=CARTESIAN_POINT('',(61.756415464215,29.,22.9997649179816));
#18669=CARTESIAN_POINT('Origin',(63.256415464215,29.,22.9997649179816));
#18670=CARTESIAN_POINT('',(61.756415464215,29.,19.4747649179816));
#18671=CARTESIAN_POINT('Origin',(63.256415464215,25.,19.4747649179816));
#18672=CARTESIAN_POINT('',(61.756415464215,25.,22.9997649179816));
#18673=CARTESIAN_POINT('Origin',(63.256415464215,25.,22.9997649179816));
#18674=CARTESIAN_POINT('',(61.756415464215,25.,19.4747649179816));
#18675=CARTESIAN_POINT('Origin',(72.5064154642151,25.,19.4747649179816));
#18676=CARTESIAN_POINT('',(71.0064154642151,25.,22.9997649179816));
#18677=CARTESIAN_POINT('Origin',(72.5064154642151,25.,22.9997649179816));
#18678=CARTESIAN_POINT('',(71.0064154642151,25.,19.4747649179816));
#18679=CARTESIAN_POINT('Origin',(67.8814154642151,21.,19.4747649179816));
#18680=CARTESIAN_POINT('',(66.3814154642151,21.,22.9997649179816));
#18681=CARTESIAN_POINT('Origin',(67.8814154642151,21.,22.9997649179816));
#18682=CARTESIAN_POINT('',(66.3814154642151,21.,19.4747649179816));
#18683=CARTESIAN_POINT('Origin',(67.8814154642151,25.,19.4747649179816));
#18684=CARTESIAN_POINT('',(66.3814154642151,25.,22.9997649179816));
#18685=CARTESIAN_POINT('Origin',(67.8814154642151,25.,22.9997649179816));
#18686=CARTESIAN_POINT('',(66.3814154642151,25.,19.4747649179816));
#18687=CARTESIAN_POINT('Origin',(63.256415464215,21.,19.4747649179816));
#18688=CARTESIAN_POINT('',(61.756415464215,21.,22.9997649179816));
#18689=CARTESIAN_POINT('Origin',(63.256415464215,21.,22.9997649179816));
#18690=CARTESIAN_POINT('',(61.756415464215,21.,19.4747649179816));
#18691=CARTESIAN_POINT('Origin',(72.5064154642151,21.,19.4747649179816));
#18692=CARTESIAN_POINT('',(71.0064154642151,21.,22.9997649179816));
#18693=CARTESIAN_POINT('Origin',(72.5064154642151,21.,22.9997649179816));
#18694=CARTESIAN_POINT('',(71.0064154642151,21.,19.4747649179816));
#18695=CARTESIAN_POINT('Origin',(58.631415464215,25.,19.4747649179816));
#18696=CARTESIAN_POINT('',(57.131415464215,25.,22.9997649179816));
#18697=CARTESIAN_POINT('Origin',(58.631415464215,25.,22.9997649179816));
#18698=CARTESIAN_POINT('',(57.131415464215,25.,19.4747649179816));
#18699=CARTESIAN_POINT('Origin',(67.8814154642151,29.,19.4747649179816));
#18700=CARTESIAN_POINT('',(66.3814154642151,29.,22.9997649179816));
#18701=CARTESIAN_POINT('Origin',(67.8814154642151,29.,22.9997649179816));
#18702=CARTESIAN_POINT('',(66.3814154642151,29.,19.4747649179816));
#18703=CARTESIAN_POINT('Origin',(60.0588019917919,32.0710678118655,19.4747649179816));
#18704=CARTESIAN_POINT('',(52.9877341799264,25.,22.9997649179816));
#18705=CARTESIAN_POINT('',(52.9877341799264,25.,19.4747649179816));
#18706=CARTESIAN_POINT('',(60.0588019917919,32.0710678118655,22.9997649179816));
#18707=CARTESIAN_POINT('',(62.8893846093759,34.9016504294496,22.9997649179816));
#18708=CARTESIAN_POINT('',(60.0588019917919,32.0710678118655,19.4747649179816));
#18709=CARTESIAN_POINT('Origin',(82.9877341799264,25.,19.4747649179816));
#18710=CARTESIAN_POINT('',(75.916666368061,32.0710678118655,22.9997649179816));
#18711=CARTESIAN_POINT('',(75.916666368061,32.0710678118655,19.4747649179816));
#18712=CARTESIAN_POINT('',(82.9877341799264,25.,22.9997649179816));
#18713=CARTESIAN_POINT('',(76.6216176564096,31.3661165235168,22.9997649179816));
#18714=CARTESIAN_POINT('',(82.9877341799264,25.,19.4747649179816));
#18715=CARTESIAN_POINT('Origin',(75.916666368061,17.9289321881345,19.4747649179816));
#18716=CARTESIAN_POINT('',(75.916666368061,17.9289321881345,22.9997649179816));
#18717=CARTESIAN_POINT('',(78.3183167975105,20.3305826175841,22.9997649179816));
#18718=CARTESIAN_POINT('',(75.916666368061,17.9289321881345,19.4747649179816));
#18719=CARTESIAN_POINT('Origin',(60.0588019917919,17.9289321881345,19.4747649179816));
#18720=CARTESIAN_POINT('',(60.0588019917919,17.9289321881345,22.9997649179816));
#18721=CARTESIAN_POINT('',(64.0232680858592,17.9289321881345,22.9997649179816));
#18722=CARTESIAN_POINT('',(60.0588019917919,17.9289321881345,19.4747649179816));
#18723=CARTESIAN_POINT('Origin',(52.9877341799264,25.,19.4747649179816));
#18724=CARTESIAN_POINT('',(54.1216176564096,23.8661165235168,22.9997649179816));
#18725=CARTESIAN_POINT('Origin',(67.9877341799264,35.4644660940673,22.9997649179816));
#18726=CARTESIAN_POINT('',(60.0588019917919,50.,22.9997649179816));
#18727=CARTESIAN_POINT('',(75.916666368061,50.,22.9997649179816));
#18728=CARTESIAN_POINT('',(71.9522002739937,50.,22.9997649179816));
#18729=CARTESIAN_POINT('',(60.0588019917919,44.2322330470336,22.9997649179816));
#18730=CARTESIAN_POINT('',(75.916666368061,33.7677669529664,22.9997649179816));
#18731=CARTESIAN_POINT('Origin',(60.0588019917919,53.,30.4747649179816));
#18732=CARTESIAN_POINT('',(60.0588019917919,53.,-0.000235082018433808));
#18733=CARTESIAN_POINT('',(60.0588019917919,53.,30.4747649179816));
#18734=CARTESIAN_POINT('',(75.916666368061,53.,-0.000235082018433808));
#18735=CARTESIAN_POINT('',(75.916666368061,53.,30.4747649179816));
#18736=CARTESIAN_POINT('',(60.0588019917919,53.,-0.000235082018433808));
#18737=CARTESIAN_POINT('Origin',(75.916666368061,50.,30.4747649179816));
#18738=CARTESIAN_POINT('',(60.0588019917919,50.,30.4747649179816));
#18739=CARTESIAN_POINT('',(75.916666368061,50.,30.4747649179816));
#18740=CARTESIAN_POINT('Origin',(60.0588019917919,50.,30.4747649179816));
#18741=CARTESIAN_POINT('',(60.0588019917919,50.,-0.000235082018433808));
#18742=CARTESIAN_POINT('',(60.0588019917919,50.,-0.000235082018433808));
#18743=CARTESIAN_POINT('',(60.0588019917919,50.,30.4747649179816));
#18744=CARTESIAN_POINT('Origin',(75.916666368061,50.,30.4747649179816));
#18745=CARTESIAN_POINT('',(75.916666368061,50.,-0.000235082018433808));
#18746=CARTESIAN_POINT('',(75.916666368061,50.,-0.000235082018433808));
#18747=CARTESIAN_POINT('',(75.916666368061,50.,30.4747649179816));
#18748=CARTESIAN_POINT('Origin',(75.916666368061,53.,30.4747649179816));
#18749=CARTESIAN_POINT('',(75.916666368061,53.,-0.000235082018433808));
#18750=CARTESIAN_POINT('Origin',(67.9877341799264,51.5,-0.000235082018433808));
#19198=UNCERTAINTY_MEASURE_WITH_UNIT(LENGTH_MEASURE(0.01),#19221,
'DISTANCE_ACCURACY_VALUE',
'Maximum model space distance between geometric entities at asserted c
onnectivities');
#19204=UNCERTAINTY_MEASURE_WITH_UNIT(LENGTH_MEASURE(0.01),#19221,
'DISTANCE_ACCURACY_VALUE',
'Maximum model space distance between geometric entities at asserted c
onnectivities');
#19214=(
GEOMETRIC_REPRESENTATION_CONTEXT(3)
GLOBAL_UNCERTAINTY_ASSIGNED_CONTEXT((#19198))
GLOBAL_UNIT_ASSIGNED_CONTEXT((#19221,#19223,#19224))
REPRESENTATION_CONTEXT('','3D')
);
#19220=(
GEOMETRIC_REPRESENTATION_CONTEXT(3)
GLOBAL_UNCERTAINTY_ASSIGNED_CONTEXT((#19204))
GLOBAL_UNIT_ASSIGNED_CONTEXT((#19221,#19223,#19224))
REPRESENTATION_CONTEXT('','3D')
);
#19221=(
LENGTH_UNIT()
NAMED_UNIT(*)
SI_UNIT(.MILLI.,.METRE.)
);
#19223=(
NAMED_UNIT(*)
PLANE_ANGLE_UNIT()
SI_UNIT($,.RADIAN.)
);
#19224=(
NAMED_UNIT(*)
SI_UNIT($,.STERADIAN.)
SOLID_ANGLE_UNIT()
);
#19234=SHAPE_DEFINITION_REPRESENTATION(#19249,#19278);
#19249=PRODUCT_DEFINITION_SHAPE('',$,#19294);
#19278=SHAPE_REPRESENTATION('',(#12488),#19214);
#19284=PRODUCT_DEFINITION_CONTEXT('part definition',#19331,'design');
#19294=PRODUCT_DEFINITION('Bracket_02 (1)','Bracket_02 (1)',#19309,#19284);
#19309=PRODUCT_DEFINITION_FORMATION('',$,#19342);
#19331=APPLICATION_CONTEXT(
'Core Data for Automotive Mechanical Design Process');
#19332=PRODUCT_CONTEXT('part definition',#19331,'mechanical');
#19342=PRODUCT('Bracket_02 (1)','Bracket_02 (1)',$,(#19332));
#19376=COLOUR_RGB('Dark Blue',0.08,0.2,0.34);
#19377=FILL_AREA_STYLE_COLOUR('',#19376);
#19378=FILL_AREA_STYLE('',(#19377));
#19379=SURFACE_STYLE_FILL_AREA(#19378);
#19380=SURFACE_SIDE_STYLE('',(#19379));
#19381=SURFACE_STYLE_USAGE(.BOTH.,#19380);
#19382=PRESENTATION_STYLE_ASSIGNMENT((#19381));
ENDSEC;
END-ISO-10303-21;
